ISO-10303-21;
HEADER;
FILE_DESCRIPTION (('STEP AP214'),
    '1' );
FILE_NAME ('Part 133_Varsay\X2\0131\X0\lan.step',
    '2026-10-08T11:03:28',
    ( '' ),
    ( '' ),
    'SwSTEP 2.0',
    'SolidWorks 2024',
    '' );
FILE_SCHEMA (( 'AUTOMOTIVE_DESIGN' ));
ENDSEC;

DATA;
#21=VERTEX_POINT ( 'NONE', #4097 ) ;
#30=ORIENTED_EDGE ( 'NONE', *, *, #51, .F. ) ;
#32=ADVANCED_FACE ( 'NONE', ( #797 ), #4451, .F. ) ;
#37=DIRECTION ( 'NONE',  ( 0.000000000000000000, -8.673617379884027583E-16, 1.000000000000000000 ) ) ;
#39=EDGE_CURVE ( 'NONE', #3048, #992, #3247, .T. ) ;
#41=DIRECTION ( 'NONE',  ( 0.000000000000000000, 1.000000000000000000, 0.000000000000000000 ) ) ;
#46=DIRECTION ( 'NONE',  ( 1.000000000000000000, -8.673617379884027583E-16, 0.000000000000000000 ) ) ;
#48=ORIENTED_EDGE ( 'NONE', *, *, #4168, .T. ) ;
#51=EDGE_CURVE ( 'NONE', #1305, #4402, #2822, .T. ) ;
#52=SURFACE_SIDE_STYLE ('',( #3578 ) ) ;
#64=SPHERICAL_SURFACE ( 'NONE', #81, 0.5000000000000000000 ) ;
#66=ORIENTED_EDGE ( 'NONE', *, *, #2001, .F. ) ;
#71=( BOUNDED_CURVE ( )  B_SPLINE_CURVE ( 3, ( #2713, #202, #1737, #3164 ),
 .UNSPECIFIED., .F., .F. ) 
 B_SPLINE_CURVE_WITH_KNOTS ( ( 4, 4 ),
 ( 0.000000000000000000, 1.570796326794896558 ),
 .UNSPECIFIED. ) 
 CURVE ( )  GEOMETRIC_REPRESENTATION_ITEM ( )  RATIONAL_B_SPLINE_CURVE ( ( 1.000000000000000000, 0.8047378541243649375, 0.8047378541243649375, 1.000000000000000000 ) ) 
 REPRESENTATION_ITEM ( '' )  );
#75=DIRECTION ( 'NONE',  ( -1.000000000000000000, -0.000000000000000000, -0.000000000000000000 ) ) ;
#76=ORIENTED_EDGE ( 'NONE', *, *, #1333, .T. ) ;
#81=AXIS2_PLACEMENT_3D ( 'NONE', #3592, #41, #3309 ) ;
#82=CARTESIAN_POINT ( 'NONE',  ( 6.586250505521797471, -10.16000000000000014, 17.78000050552179445 ) ) ;
#85=DIRECTION ( 'NONE',  ( 0.000000000000000000, 0.000000000000000000, 1.000000000000000000 ) ) ;
#86=CARTESIAN_POINT ( 'NONE',  ( 17.28000050552179800, -17.28000000000000114, 17.78000050552179445 ) ) ;
#89=SPHERICAL_SURFACE ( 'NONE', #874, 0.5000000000000000000 ) ;
#90=ADVANCED_FACE ( 'NONE', ( #3987 ), #2494, .T. ) ;
#92=DIRECTION ( 'NONE',  ( 1.707404996040164265E-16, -1.000000000000000000, 0.000000000000000000 ) ) ;
#109=CARTESIAN_POINT ( 'NONE',  ( 10.16000050552179701, -10.16000000000000014, 17.78000050552179445 ) ) ;
#110=ORIENTED_EDGE ( 'NONE', *, *, #3169, .F. ) ;
#118=DIRECTION ( 'NONE',  ( 0.000000000000000000, 0.000000000000000000, -1.000000000000000000 ) ) ;
#129=DIRECTION ( 'NONE',  ( 0.000000000000000000, 0.000000000000000000, 1.000000000000000000 ) ) ;
#133=ORIENTED_EDGE ( 'NONE', *, *, #4375, .F. ) ;
#136=AXIS2_PLACEMENT_3D ( 'NONE', #1284, #2724, #2568 ) ;
#139=CARTESIAN_POINT ( 'NONE',  ( 12.25345478699094670, -6.586249999999999716, 12.25345478699094670 ) ) ;
#150=ORIENTED_EDGE ( 'NONE', *, *, #1875, .T. ) ;
#158=EDGE_CURVE ( 'NONE', #2359, #3396, #1229, .T. ) ;
#172=ORIENTED_EDGE ( 'NONE', *, *, #2866, .T. ) ;
#177=EDGE_CURVE ( 'NONE', #3571, #1450, #388, .T. ) ;
#179=CARTESIAN_POINT ( 'NONE',  ( 10.16000050552179701, -6.586249999999999716, 10.16000050552179701 ) ) ;
#186=CARTESIAN_POINT ( 'NONE',  ( 17.28000050552179445, -3.039999999999999591, 17.28000050552179445 ) ) ;
#188=FACE_OUTER_BOUND ( 'NONE', #2341, .T. ) ;
#190=ORIENTED_EDGE ( 'NONE', *, *, #2135, .T. ) ;
#193=DIRECTION ( 'NONE',  ( -1.000000000000000000, -0.000000000000000000, -0.000000000000000000 ) ) ;
#196=ORIENTED_EDGE ( 'NONE', *, *, #2432, .T. ) ;
#198=AXIS2_PLACEMENT_3D ( 'NONE', #939, #3484, #1720 ) ;
#202=CARTESIAN_POINT ( 'NONE',  ( 6.586250505521797471, -12.25345428146915161, 6.586250505521797471 ) ) ;
#214=ORIENTED_EDGE ( 'NONE', *, *, #499, .T. ) ;
#215=DIRECTION ( 'NONE',  ( -1.000000000000000000, 8.673617379884035472E-16, -8.673617379884035472E-16 ) ) ;
#221=AXIS2_PLACEMENT_3D ( 'NONE', #1438, #2596, #3615 ) ;
#223=SPHERICAL_SURFACE ( 'NONE', #1597, 0.5000000000000000000 ) ;
#229=LINE ( 'NONE', #603, #348 ) ;
#232=AXIS2_PLACEMENT_3D ( 'NONE', #4351, #46, #1908 ) ;
#237=DIRECTION ( 'NONE',  ( 0.000000000000000000, 0.000000000000000000, -1.000000000000000000 ) ) ;
#240=AXIS2_PLACEMENT_3D ( 'NONE', #4426, #2657, #1612 ) ;
#241=ORIENTED_EDGE ( 'NONE', *, *, #1369, .F. ) ;
#242=ORIENTED_EDGE ( 'NONE', *, *, #4335, .T. ) ;
#245=VERTEX_POINT ( 'NONE', #3401 ) ;
#249=CARTESIAN_POINT ( 'NONE',  ( 2.540000505521796015, -3.039999999999999147, 17.78000050552179445 ) ) ;
#253=CYLINDRICAL_SURFACE ( 'NONE', #2742, 3.573749999999999538 ) ;
#256=AXIS2_PLACEMENT_3D ( 'NONE', #4355, #1062, #678 ) ;
#257=ORIENTED_EDGE ( 'NONE', *, *, #1303, .F. ) ;
#267=ORIENTED_EDGE ( 'NONE', *, *, #1508, .F. ) ;
#268=LINE ( 'NONE', #2393, #3299 ) ;
#282=ORIENTED_EDGE ( 'NONE', *, *, #177, .F. ) ;
#285=VECTOR ( 'NONE', #339, 1000.000000000000000 ) ;
#294=DIRECTION ( 'NONE',  ( -0.000000000000000000, 1.000000000000000000, 0.000000000000000000 ) ) ;
#295=( GEOMETRIC_REPRESENTATION_CONTEXT ( 3 ) GLOBAL_UNCERTAINTY_ASSIGNED_CONTEXT ( ( #2687 ) ) GLOBAL_UNIT_ASSIGNED_CONTEXT ( ( #3953, #4645, #1803 ) ) REPRESENTATION_CONTEXT ( 'NONE', 'WORKASPACE' ) );
#307=CIRCLE ( 'NONE', #4141, 0.5000000000000004441 ) ;
#309=AXIS2_PLACEMENT_3D ( 'NONE', #1170, #75, #1587 ) ;
#319=LINE ( 'NONE', #249, #4138 ) ;
#320=CYLINDRICAL_SURFACE ( 'NONE', #2187, 0.5000000000000000000 ) ;
#330=ORIENTED_EDGE ( 'NONE', *, *, #3902, .T. ) ;
#332=VECTOR ( 'NONE', #1088, 1000.000000000000000 ) ;
#336=ORIENTED_EDGE ( 'NONE', *, *, #4404, .T. ) ;
#339=DIRECTION ( 'NONE',  ( -1.000000000000000000, -0.000000000000000000, -0.000000000000000000 ) ) ;
#343=CARTESIAN_POINT ( 'NONE',  ( 6.586250505521797471, -10.16000000000000014, 17.78000050552179445 ) ) ;
#344=EDGE_CURVE ( 'NONE', #4402, #4095, #478, .T. ) ;
#348=VECTOR ( 'NONE', #1681, 1000.000000000000000 ) ;
#355=EDGE_LOOP ( 'NONE', ( #267, #1778 ) ) ;
#356=VERTEX_POINT ( 'NONE', #2750 ) ;
#357=PRESENTATION_STYLE_ASSIGNMENT (( #1496 ) ) ;
#361=EDGE_CURVE ( 'NONE', #3625, #1713, #3063, .T. ) ;
#362=CARTESIAN_POINT ( 'NONE',  ( 2.540000505521796015, -10.16000000000000014, 10.16000050552179701 ) ) ;
#374=DIRECTION ( 'NONE',  ( 0.000000000000000000, -1.000000000000000000, 0.000000000000000000 ) ) ;
#377=SPHERICAL_SURFACE ( 'NONE', #256, 0.5000000000000000000 ) ;
#381=EDGE_CURVE ( 'NONE', #1044, #2857, #1512, .T. ) ;
#382=EDGE_LOOP ( 'NONE', ( #2847, #4617 ) ) ;
#383=ORIENTED_EDGE ( 'NONE', *, *, #467, .F. ) ;
#386=VECTOR ( 'NONE', #4108, 1000.000000000000000 ) ;
#388=CIRCLE ( 'NONE', #2641, 0.5000000000000004441 ) ;
#390=DIRECTION ( 'NONE',  ( 1.000000000000000000, 0.000000000000000000, 0.000000000000000000 ) ) ;
#391=MANIFOLD_SOLID_BREP ( 'Radyus1', #3647 ) ;
#402=ORIENTED_EDGE ( 'NONE', *, *, #4582, .T. ) ;
#403=EDGE_LOOP ( 'NONE', ( #3744, #2182 ) ) ;
#413=DIRECTION ( 'NONE',  ( -1.000000000000000000, -0.000000000000000000, -0.000000000000000000 ) ) ;
#419=AXIS2_PLACEMENT_3D ( 'NONE', #582, #2380, #2739 ) ;
#423=CARTESIAN_POINT ( 'NONE',  ( 17.78000050552179445, -10.16000000000000014, 10.16000050552179701 ) ) ;
#424=EDGE_CURVE ( 'NONE', #356, #3559, #902, .T. ) ;
#432=CARTESIAN_POINT ( 'NONE',  ( 6.586250505521797471, -8.066545718530848674, 6.586250505521797471 ) ) ;
#443=EDGE_LOOP ( 'NONE', ( #2753, #3813, #2295, #1561, #4044 ) ) ;
#444=DIRECTION ( 'NONE',  ( -1.707404996040164265E-16, 1.000000000000000000, 0.000000000000000000 ) ) ;
#456=EDGE_CURVE ( 'NONE', #1954, #992, #4200, .T. ) ;
#458=( NAMED_UNIT ( * ) SI_UNIT ( $, .STERADIAN. ) SOLID_ANGLE_UNIT ( ) );
#467=EDGE_CURVE ( 'NONE', #4067, #3625, #2172, .T. ) ;
#468=VECTOR ( 'NONE', #4539, 1000.000000000000000 ) ;
#476=ORIENTED_EDGE ( 'NONE', *, *, #865, .F. ) ;
#478=( BOUNDED_CURVE ( )  B_SPLINE_CURVE ( 3, ( #2081, #2730, #3495, #2370 ),
 .UNSPECIFIED., .F., .T. ) 
 B_SPLINE_CURVE_WITH_KNOTS ( ( 4, 4 ),
 ( 0.000000000000000000, 1.570796326794896558 ),
 .UNSPECIFIED. ) 
 CURVE ( )  GEOMETRIC_REPRESENTATION_ITEM ( )  RATIONAL_B_SPLINE_CURVE ( ( 1.000000000000000000, 0.8047378541243649375, 0.8047378541243649375, 1.000000000000000000 ) ) 
 REPRESENTATION_ITEM ( '' )  );
#480=ORIENTED_EDGE ( 'NONE', *, *, #3902, .F. ) ;
#481=FACE_OUTER_BOUND ( 'NONE', #1065, .T. ) ;
#490=DIRECTION ( 'NONE',  ( 0.000000000000000000, 0.000000000000000000, -1.000000000000000000 ) ) ;
#499=EDGE_CURVE ( 'NONE', #1954, #3048, #2558, .T. ) ;
#505=EDGE_CURVE ( 'NONE', #3774, #4040, #537, .T. ) ;
#508=LINE ( 'NONE', #934, #679 ) ;
#519=DIRECTION ( 'NONE',  ( 0.000000000000000000, 0.000000000000000000, -1.000000000000000000 ) ) ;
#524=ORIENTED_EDGE ( 'NONE', *, *, #4084, .T. ) ;
#531=DIRECTION ( 'NONE',  ( 0.000000000000000000, 0.000000000000000000, 1.000000000000000000 ) ) ;
#533=AXIS2_PLACEMENT_3D ( 'NONE', #3219, #2856, #2427 ) ;
#536=CARTESIAN_POINT ( 'NONE',  ( 2.540000505521796015, -2.539999999999999591, 17.28000050552179445 ) ) ;
#537=CIRCLE ( 'NONE', #309, 0.5000000000000000000 ) ;
#538=ORIENTED_EDGE ( 'NONE', *, *, #3424, .F. ) ;
#542=EDGE_CURVE ( 'NONE', #3954, #2747, #3742, .T. ) ;
#566=VERTEX_POINT ( 'NONE', #1263 ) ;
#573=ADVANCED_FACE ( 'NONE', ( #4118 ), #2319, .F. ) ;
#582=CARTESIAN_POINT ( 'NONE',  ( 17.28000050552179445, -3.039999999999999591, 17.28000050552179445 ) ) ;
#585=DIRECTION ( 'NONE',  ( -8.673617379884035472E-16, -1.000000000000000000, -0.000000000000000000 ) ) ;
#588=ORIENTED_EDGE ( 'NONE', *, *, #2678, .T. ) ;
#603=CARTESIAN_POINT ( 'NONE',  ( 17.78000050552179445, -10.16000000000000014, 13.73375050552179744 ) ) ;
#606=EDGE_CURVE ( 'NONE', #1954, #21, #4612, .T. ) ;
#607=CIRCLE ( 'NONE', #3547, 0.5000000000000004441 ) ;
#612=CARTESIAN_POINT ( 'NONE',  ( 3.040000505521796015, -2.539999999999999591, 17.28000050552179445 ) ) ;
#619=DIRECTION ( 'NONE',  ( -0.000000000000000000, 1.000000000000000000, -0.000000000000000000 ) ) ;
#626=FACE_OUTER_BOUND ( 'NONE', #1636, .T. ) ;
#633=ORIENTED_EDGE ( 'NONE', *, *, #3448, .F. ) ;
#635=EDGE_LOOP ( 'NONE', ( #3645, #633, #1686, #3639, #3220 ) ) ;
#649=CARTESIAN_POINT ( 'NONE',  ( 3.040000505521796015, -17.28000000000000114, 17.78000050552179445 ) ) ;
#653=ORIENTED_EDGE ( 'NONE', *, *, #499, .F. ) ;
#667=EDGE_CURVE ( 'NONE', #3496, #2728, #3377, .T. ) ;
#673=DIRECTION ( 'NONE',  ( 0.000000000000000000, 0.000000000000000000, 1.000000000000000000 ) ) ;
#678=DIRECTION ( 'NONE',  ( 0.000000000000000000, 0.000000000000000000, -1.000000000000000000 ) ) ;
#679=VECTOR ( 'NONE', #2972, 1000.000000000000000 ) ;
#692=DIRECTION ( 'NONE',  ( -0.000000000000000000, -0.000000000000000000, -1.000000000000000000 ) ) ;
#706=DIRECTION ( 'NONE',  ( -1.000000000000000000, 0.000000000000000000, 0.000000000000000000 ) ) ;
#707=EDGE_LOOP ( 'NONE', ( #524, #3331, #1259 ) ) ;
#712=EDGE_CURVE ( 'NONE', #566, #2813, #3871, .T. ) ;
#716=DIRECTION ( 'NONE',  ( 1.707404996040164265E-16, -1.000000000000000000, -0.000000000000000000 ) ) ;
#722=AXIS2_PLACEMENT_3D ( 'NONE', #3419, #193, #1172 ) ;
#729=DIRECTION ( 'NONE',  ( -1.000000000000000000, 0.000000000000000000, 0.000000000000000000 ) ) ;
#732=CIRCLE ( 'NONE', #2241, 0.5000000000000000000 ) ;
#742=PLANE ( 'NONE',  #2974 ) ;
#749=CIRCLE ( 'NONE', #3983, 0.5000000000000004441 ) ;
#762=CYLINDRICAL_SURFACE ( 'NONE', #4557, 0.5000000000000004441 ) ;
#763=DIRECTION ( 'NONE',  ( 0.000000000000000000, 0.000000000000000000, 1.000000000000000000 ) ) ;
#765=DIRECTION ( 'NONE',  ( 0.000000000000000000, 0.000000000000000000, -1.000000000000000000 ) ) ;
#766=ORIENTED_EDGE ( 'NONE', *, *, #3357, .F. ) ;
#770=VECTOR ( 'NONE', #3536, 1000.000000000000000 ) ;
#778=PRODUCT_CONTEXT ( 'NONE', #1536, 'mechanical' ) ;
#784=ADVANCED_FACE ( 'NONE', ( #785 ), #64, .T. ) ;
#785=FACE_OUTER_BOUND ( 'NONE', #2617, .T. ) ;
#786=FACE_OUTER_BOUND ( 'NONE', #4051, .T. ) ;
#790=CIRCLE ( 'NONE', #198, 0.5000000000000000000 ) ;
#797=FACE_OUTER_BOUND ( 'NONE', #2697, .T. ) ;
#800=DIRECTION ( 'NONE',  ( -1.000000000000000000, 0.000000000000000000, 0.000000000000000000 ) ) ;
#813=AXIS2_PLACEMENT_3D ( 'NONE', #362, #729, #1021 ) ;
#830=CARTESIAN_POINT ( 'NONE',  ( 17.28000050552179800, -17.28000000000000114, 3.040000505521796015 ) ) ;
#832=SHAPE_REPRESENTATION_RELATIONSHIP ( 'NONE' , 'NONE' ,  #2003, #2068 ) ;
#844=DIRECTION ( 'NONE',  ( -1.000000000000000000, 0.000000000000000000, 0.000000000000000000 ) ) ;
#845=DIRECTION ( 'NONE',  ( -1.000000000000000000, 0.000000000000000000, 0.000000000000000000 ) ) ;
#850=ORIENTED_EDGE ( 'NONE', *, *, #667, .T. ) ;
#859=( NAMED_UNIT ( * ) PLANE_ANGLE_UNIT ( ) SI_UNIT ( $, .RADIAN. ) );
#863=ORIENTED_EDGE ( 'NONE', *, *, #344, .F. ) ;
#865=EDGE_CURVE ( 'NONE', #3460, #1305, #1452, .T. ) ;
#869=CARTESIAN_POINT ( 'NONE',  ( 13.73375050552179566, -8.066545718530848674, 13.73375050552179566 ) ) ;
#874=AXIS2_PLACEMENT_3D ( 'NONE', #2902, #1555, #1883 ) ;
#875=ORIENTED_EDGE ( 'NONE', *, *, #1369, .T. ) ;
#876=ORIENTED_EDGE ( 'NONE', *, *, #542, .F. ) ;
#884=CARTESIAN_POINT ( 'NONE',  ( 17.28000050552179800, -17.78000000000000114, 17.28000050552179445 ) ) ;
#896=EDGE_LOOP ( 'NONE', ( #76, #2578, #3022, #2141 ) ) ;
#902=CIRCLE ( 'NONE', #4130, 0.5000000000000000000 ) ;
#909=DIRECTION ( 'NONE',  ( 0.000000000000000000, 8.673617379884035472E-16, 1.000000000000000000 ) ) ;
#918=VECTOR ( 'NONE', #1102, 1000.000000000000000 ) ;
#927=ORIENTED_EDGE ( 'NONE', *, *, #2777, .T. ) ;
#929=CARTESIAN_POINT ( 'NONE',  ( 2.540000505521796015, -17.28000000000000114, 17.28000050552179445 ) ) ;
#931=DIRECTION ( 'NONE',  ( 1.000000000000000000, -0.000000000000000000, 0.000000000000000000 ) ) ;
#934=CARTESIAN_POINT ( 'NONE',  ( 2.540000505521796015, -17.28000000000000114, 17.78000050552179445 ) ) ;
#939=CARTESIAN_POINT ( 'NONE',  ( 3.040000505521796015, -3.039999999999999591, 3.040000505521795571 ) ) ;
#941=CARTESIAN_POINT ( 'NONE',  ( 2.540000505521796015, -3.039999999999999591, 3.040000505521795571 ) ) ;
#943=DIRECTION ( 'NONE',  ( 0.000000000000000000, 0.000000000000000000, -1.000000000000000000 ) ) ;
#945=DIRECTION ( 'NONE',  ( 0.000000000000000000, -0.000000000000000000, -1.000000000000000000 ) ) ;
#955=AXIS2_PLACEMENT_3D ( 'NONE', #4045, #490, #4449 ) ;
#960=AXIS2_PLACEMENT_3D ( 'NONE', #2587, #2681, #800 ) ;
#961=EDGE_CURVE ( 'NONE', #2245, #356, #319, .T. ) ;
#975=VERTEX_POINT ( 'NONE', #3121 ) ;
#976=CARTESIAN_POINT ( 'NONE',  ( 17.78000050552179800, -17.28000000000000114, 17.28000050552179445 ) ) ;
#979=LINE ( 'NONE', #2086, #4508 ) ;
#983=CARTESIAN_POINT ( 'NONE',  ( 2.540000505521796015, -10.16000000000000014, 13.73375050552179744 ) ) ;
#990=CYLINDRICAL_SURFACE ( 'NONE', #3958, 0.5000000000000004441 ) ;
#992=VERTEX_POINT ( 'NONE', #3890 ) ;
#1011=DIRECTION ( 'NONE',  ( -1.000000000000000000, 0.000000000000000000, 0.000000000000000000 ) ) ;
#1012=DIRECTION ( 'NONE',  ( 1.000000000000000000, 0.000000000000000000, 0.000000000000000000 ) ) ;
#1013=ADVANCED_FACE ( 'NONE', ( #3237 ), #2230, .T. ) ;
#1021=DIRECTION ( 'NONE',  ( 0.000000000000000000, 0.000000000000000000, 1.000000000000000000 ) ) ;
#1023=CIRCLE ( 'NONE', #3047, 3.573750000000000426 ) ;
#1033=CARTESIAN_POINT ( 'NONE',  ( 6.586250505521797471, -10.16000000000000014, 13.73375050552179744 ) ) ;
#1036=ORIENTED_EDGE ( 'NONE', *, *, #3500, .T. ) ;
#1038=AXIS2_PLACEMENT_3D ( 'NONE', #2839, #1329, #237 ) ;
#1039=CARTESIAN_POINT ( 'NONE',  ( 2.540000505521796015, -3.039999999999999591, 17.78000050552179445 ) ) ;
#1044=VERTEX_POINT ( 'NONE', #2905 ) ;
#1048=CARTESIAN_POINT ( 'NONE',  ( 17.28000050552179445, -2.539999999999999591, 3.040000505521795571 ) ) ;
#1053=DIRECTION ( 'NONE',  ( 1.000000000000000000, 0.000000000000000000, 0.000000000000000000 ) ) ;
#1062=DIRECTION ( 'NONE',  ( 0.000000000000000000, 1.000000000000000000, 0.000000000000000000 ) ) ;
#1065=EDGE_LOOP ( 'NONE', ( #1455, #336, #1469 ) ) ;
#1066=ORIENTED_EDGE ( 'NONE', *, *, #39, .F. ) ;
#1088=DIRECTION ( 'NONE',  ( 1.000000000000000000, 0.000000000000000000, 0.000000000000000000 ) ) ;
#1101=DIRECTION ( 'NONE',  ( -0.000000000000000000, 1.000000000000000000, 0.000000000000000000 ) ) ;
#1102=DIRECTION ( 'NONE',  ( 1.000000000000000000, -0.000000000000000000, -0.000000000000000000 ) ) ;
#1107=CIRCLE ( 'NONE', #1710, 3.573750000000000426 ) ;
#1122=AXIS2_PLACEMENT_3D ( 'NONE', #3295, #4378, #92 ) ;
#1128=DIRECTION ( 'NONE',  ( -0.000000000000000000, -0.000000000000000000, -1.000000000000000000 ) ) ;
#1135=CARTESIAN_POINT ( 'NONE',  ( 3.040000505521796015, -3.039999999999999147, 17.78000050552179445 ) ) ;
#1138=ORIENTED_EDGE ( 'NONE', *, *, #3783, .T. ) ;
#1146=VECTOR ( 'NONE', #3344, 1000.000000000000000 ) ;
#1156=LINE ( 'NONE', #82, #3283 ) ;
#1163=ORIENTED_EDGE ( 'NONE', *, *, #4168, .F. ) ;
#1169=CARTESIAN_POINT ( 'NONE',  ( 2.540000505521796015, -3.039999999999999591, 17.28000050552179445 ) ) ;
#1170=CARTESIAN_POINT ( 'NONE',  ( 17.28000050552179445, -3.039999999999999591, 3.040000505521796015 ) ) ;
#1172=DIRECTION ( 'NONE',  ( 0.000000000000000000, 0.000000000000000000, 1.000000000000000000 ) ) ;
#1175=LINE ( 'NONE', #3082, #1353 ) ;
#1178=ORIENTED_EDGE ( 'NONE', *, *, #1312, .T. ) ;
#1183=CARTESIAN_POINT ( 'NONE',  ( 2.540000505521796015, -2.539999999999999591, 2.540000505521796015 ) ) ;
#1193=VECTOR ( 'NONE', #3110, 1000.000000000000000 ) ;
#1194=CARTESIAN_POINT ( 'NONE',  ( 17.78000050552179445, -3.039999999999999591, 17.28000050552179445 ) ) ;
#1200=ORIENTED_EDGE ( 'NONE', *, *, #1312, .F. ) ;
#1203=DIRECTION ( 'NONE',  ( -0.000000000000000000, -0.000000000000000000, -1.000000000000000000 ) ) ;
#1214=CARTESIAN_POINT ( 'NONE',  ( 13.73375050552179566, -12.25345428146915161, 6.586250505521797471 ) ) ;
#1224=CARTESIAN_POINT ( 'NONE',  ( 6.586250505521797471, -10.16000000000000014, 6.586250505521798360 ) ) ;
#1229=CIRCLE ( 'NONE', #1453, 3.573749999999999538 ) ;
#1230=ADVANCED_FACE ( 'NONE', ( #188, #3760 ), #1634, .F. ) ;
#1238=PRODUCT_DEFINITION_CONTEXT ( 'detailed design', #3989, 'design' ) ;
#1252=DIRECTION ( 'NONE',  ( 0.000000000000000000, 0.000000000000000000, -1.000000000000000000 ) ) ;
#1255=ADVANCED_FACE ( 'NONE', ( #2721 ), #4164, .T. ) ;
#1256=CARTESIAN_POINT ( 'NONE',  ( 6.586250505521797471, -10.16000000000000014, 13.73375050552179744 ) ) ;
#1259=ORIENTED_EDGE ( 'NONE', *, *, #2962, .F. ) ;
#1263=CARTESIAN_POINT ( 'NONE',  ( 6.586250505521797471, -10.16000000000000014, 6.586250505521798360 ) ) ;
#1265=ORIENTED_EDGE ( 'NONE', *, *, #2797, .T. ) ;
#1267=LINE ( 'NONE', #1988, #3618 ) ;
#1271=FACE_BOUND ( 'NONE', #403, .T. ) ;
#1279=DIRECTION ( 'NONE',  ( 1.000000000000000000, 0.000000000000000000, 0.000000000000000000 ) ) ;
#1284=CARTESIAN_POINT ( 'NONE',  ( 17.28000050552179800, -17.28000000000000114, 17.78000050552179445 ) ) ;
#1285=CIRCLE ( 'NONE', #221, 3.573749999999999538 ) ;
#1288=EDGE_LOOP ( 'NONE', ( #4190, #66, #1066, #1381 ) ) ;
#1303=EDGE_CURVE ( 'NONE', #2728, #3460, #2764, .T. ) ;
#1305=VERTEX_POINT ( 'NONE', #4561 ) ;
#1306=CARTESIAN_POINT ( 'NONE',  ( 2.540000505521796015, -2.539999999999999591, 17.78000050552179445 ) ) ;
#1311=CARTESIAN_POINT ( 'NONE',  ( 3.040000505521796015, -3.039999999999999591, 3.040000505521796015 ) ) ;
#1312=EDGE_CURVE ( 'NONE', #1305, #4255, #1928, .T. ) ;
#1313=CARTESIAN_POINT ( 'NONE',  ( 17.28000050552179800, -17.28000000000000114, 17.28000050552179445 ) ) ;
#1324=DIRECTION ( 'NONE',  ( 0.000000000000000000, 0.000000000000000000, -1.000000000000000000 ) ) ;
#1327=CARTESIAN_POINT ( 'NONE',  ( 17.78000050552179445, -10.16000000000000014, 13.73375050552179744 ) ) ;
#1329=DIRECTION ( 'NONE',  ( -1.000000000000000000, -0.000000000000000000, 0.000000000000000000 ) ) ;
#1333=EDGE_CURVE ( 'NONE', #3048, #3625, #4204, .T. ) ;
#1343=DIRECTION ( 'NONE',  ( 1.000000000000000000, 0.000000000000000000, 0.000000000000000000 ) ) ;
#1351=VERTEX_POINT ( 'NONE', #983 ) ;
#1353=VECTOR ( 'NONE', #943, 1000.000000000000000 ) ;
#1354=EDGE_CURVE ( 'NONE', #4402, #1044, #3919, .T. ) ;
#1368=VECTOR ( 'NONE', #2406, 1000.000000000000000 ) ;
#1369=EDGE_CURVE ( 'NONE', #1649, #245, #749, .T. ) ;
#1371=CARTESIAN_POINT ( 'NONE',  ( 17.78000050552179445, -10.16000000000000014, 10.16000050552179701 ) ) ;
#1373=DIRECTION ( 'NONE',  ( 1.000000000000000000, -0.000000000000000000, 0.000000000000000000 ) ) ;
#1381=ORIENTED_EDGE ( 'NONE', *, *, #1992, .F. ) ;
#1383=ADVANCED_FACE ( 'NONE', ( #2382 ), #3146, .F. ) ;
#1387=CYLINDRICAL_SURFACE ( 'NONE', #4119, 0.5000000000000004441 ) ;
#1390=DIRECTION ( 'NONE',  ( 0.000000000000000000, 0.000000000000000000, -1.000000000000000000 ) ) ;
#1405=FILL_AREA_STYLE_COLOUR ( '', #1957 ) ;
#1407=CYLINDRICAL_SURFACE ( 'NONE', #3652, 0.5000000000000004441 ) ;
#1409=FACE_OUTER_BOUND ( 'NONE', #4356, .T. ) ;
#1416=DIRECTION ( 'NONE',  ( -1.000000000000000000, 0.000000000000000000, 0.000000000000000000 ) ) ;
#1422=EDGE_LOOP ( 'NONE', ( #2723, #2332, #3770, #766 ) ) ;
#1423=CARTESIAN_POINT ( 'NONE',  ( 17.78000050552179445, -3.039999999999999591, 3.040000505521795571 ) ) ;
#1426=CARTESIAN_POINT ( 'NONE',  ( 17.28000050552179800, -17.28000000000000114, 3.040000505521795571 ) ) ;
#1431=DIRECTION ( 'NONE',  ( 0.000000000000000000, 1.000000000000000000, 0.000000000000000000 ) ) ;
#1433=LINE ( 'NONE', #3562, #285 ) ;
#1436=CARTESIAN_POINT ( 'NONE',  ( 17.78000050552179445, -3.039999999999999591, 2.540000505521796015 ) ) ;
#1438=CARTESIAN_POINT ( 'NONE',  ( 10.16000050552179701, -10.16000000000000014, 2.540000505521796015 ) ) ;
#1442=PLANE ( 'NONE',  #1122 ) ;
#1449=EDGE_CURVE ( 'NONE', #4040, #3180, #4344, .T. ) ;
#1450=VERTEX_POINT ( 'NONE', #86 ) ;
#1452=( BOUNDED_CURVE ( )  B_SPLINE_CURVE ( 3, ( #3043, #2623, #3095, #3456 ),
 .UNSPECIFIED., .F., .T. ) 
 B_SPLINE_CURVE_WITH_KNOTS ( ( 4, 4 ),
 ( 3.141592653589793116, 4.712388980384689674 ),
 .UNSPECIFIED. ) 
 CURVE ( )  GEOMETRIC_REPRESENTATION_ITEM ( )  RATIONAL_B_SPLINE_CURVE ( ( 1.000000000000000000, 0.8047378541243649375, 0.8047378541243649375, 1.000000000000000000 ) ) 
 REPRESENTATION_ITEM ( '' )  );
#1453=AXIS2_PLACEMENT_3D ( 'NONE', #4055, #1648, #3722 ) ;
#1455=ORIENTED_EDGE ( 'NONE', *, *, #424, .T. ) ;
#1464=CARTESIAN_POINT ( 'NONE',  ( 13.73375050552179744, -10.16000000000000014, 17.78000050552179445 ) ) ;
#1469=ORIENTED_EDGE ( 'NONE', *, *, #3883, .F. ) ;
#1471=CIRCLE ( 'NONE', #4088, 0.5000000000000000000 ) ;
#1473=DIRECTION ( 'NONE',  ( -1.707404996040164265E-16, 1.000000000000000000, 0.000000000000000000 ) ) ;
#1486=CARTESIAN_POINT ( 'NONE',  ( 3.040000505521796015, -2.539999999999999591, 17.78000050552179445 ) ) ;
#1493=ORIENTED_EDGE ( 'NONE', *, *, #606, .F. ) ;
#1496=SURFACE_STYLE_USAGE ( .BOTH. , #52 ) ;
#1508=EDGE_CURVE ( 'NONE', #2857, #1044, #1285, .T. ) ;
#1512=CIRCLE ( 'NONE', #3154, 3.573749999999999538 ) ;
#1517=ADVANCED_FACE ( 'NONE', ( #2947 ), #2499, .F. ) ;
#1526=ORIENTED_EDGE ( 'NONE', *, *, #3586, .F. ) ;
#1536=APPLICATION_CONTEXT ( 'automotive_design' ) ;
#1544=CARTESIAN_POINT ( 'NONE',  ( 3.040000505521796015, -17.28000000000000114, 3.040000505521795571 ) ) ;
#1546=EDGE_LOOP ( 'NONE', ( #4103, #190, #1578 ) ) ;
#1550=LINE ( 'NONE', #4487, #1751 ) ;
#1555=DIRECTION ( 'NONE',  ( 0.000000000000000000, 1.000000000000000000, 0.000000000000000000 ) ) ;
#1561=ORIENTED_EDGE ( 'NONE', *, *, #2866, .F. ) ;
#1562=CARTESIAN_POINT ( 'NONE',  ( 10.16000050552179701, -6.586249999999999716, 10.16000050552179701 ) ) ;
#1565=CARTESIAN_POINT ( 'NONE',  ( 10.16000050552179701, -13.73374999999999879, 10.16000050552179701 ) ) ;
#1568=ORIENTED_EDGE ( 'NONE', *, *, #4582, .F. ) ;
#1572=EDGE_LOOP ( 'NONE', ( #150, #1682, #4239, #3493 ) ) ;
#1578=ORIENTED_EDGE ( 'NONE', *, *, #3298, .F. ) ;
#1581=STYLED_ITEM ( 'NONE', ( #357 ), #391 ) ;
#1587=DIRECTION ( 'NONE',  ( 0.000000000000000000, 0.000000000000000000, -1.000000000000000000 ) ) ;
#1594=CARTESIAN_POINT ( 'NONE',  ( 17.28000050552179800, -17.28000000000000114, 17.28000050552179445 ) ) ;
#1595=ADVANCED_FACE ( 'NONE', ( #3680 ), #4415, .F. ) ;
#1597=AXIS2_PLACEMENT_3D ( 'NONE', #2350, #931, #909 ) ;
#1599=CIRCLE ( 'NONE', #1891, 0.5000000000000004441 ) ;
#1602=DIRECTION ( 'NONE',  ( -1.000000000000000000, 0.000000000000000000, 0.000000000000000000 ) ) ;
#1609=ORIENTED_EDGE ( 'NONE', *, *, #4619, .T. ) ;
#1611=FACE_OUTER_BOUND ( 'NONE', #1911, .T. ) ;
#1612=DIRECTION ( 'NONE',  ( -1.000000000000000000, 0.000000000000000000, 0.000000000000000000 ) ) ;
#1615=CARTESIAN_POINT ( 'NONE',  ( 17.28000050552179445, -2.539999999999996927, 17.78000050552179445 ) ) ;
#1616=ORIENTED_EDGE ( 'NONE', *, *, #542, .T. ) ;
#1622=UNCERTAINTY_MEASURE_WITH_UNIT (LENGTH_MEASURE( 1.000000000000000082E-05 ), #4035, 'distance_accuracy_value', 'NONE');
#1624=CARTESIAN_POINT ( 'NONE',  ( 17.78000050552179445, -10.16000000000000014, 6.586250505521796583 ) ) ;
#1634=PLANE ( 'NONE',  #4302 ) ;
#1636=EDGE_LOOP ( 'NONE', ( #2095, #4455, #30, #476, #257 ) ) ;
#1637=CIRCLE ( 'NONE', #419, 0.5000000000000004441 ) ;
#1640=PRODUCT_DEFINITION ( 'UNKNOWN', '', #4328, #1238 ) ;
#1642=FACE_OUTER_BOUND ( 'NONE', #2512, .T. ) ;
#1647=VECTOR ( 'NONE', #1977, 1000.000000000000000 ) ;
#1648=DIRECTION ( 'NONE',  ( 0.000000000000000000, 0.000000000000000000, -1.000000000000000000 ) ) ;
#1649=VERTEX_POINT ( 'NONE', #2309 ) ;
#1658=DIRECTION ( 'NONE',  ( 0.000000000000000000, -0.000000000000000000, -1.000000000000000000 ) ) ;
#1659=ORIENTED_EDGE ( 'NONE', *, *, #1354, .F. ) ;
#1669=ORIENTED_EDGE ( 'NONE', *, *, #3593, .F. ) ;
#1681=DIRECTION ( 'NONE',  ( -1.000000000000000000, -0.000000000000000000, -0.000000000000000000 ) ) ;
#1682=ORIENTED_EDGE ( 'NONE', *, *, #606, .T. ) ;
#1686=ORIENTED_EDGE ( 'NONE', *, *, #2727, .F. ) ;
#1694=FACE_OUTER_BOUND ( 'NONE', #1422, .T. ) ;
#1701=CARTESIAN_POINT ( 'NONE',  ( 3.040000505521795571, -17.78000000000000114, 17.28000050552179445 ) ) ;
#1710=AXIS2_PLACEMENT_3D ( 'NONE', #2132, #1813, #2498 ) ;
#1712=CIRCLE ( 'NONE', #955, 0.5000000000000004441 ) ;
#1713=VERTEX_POINT ( 'NONE', #884 ) ;
#1720=DIRECTION ( 'NONE',  ( 0.000000000000000000, 0.000000000000000000, 1.000000000000000000 ) ) ;
#1721=CARTESIAN_POINT ( 'NONE',  ( 17.28000050552179445, -3.039999999999999591, 17.28000050552179445 ) ) ;
#1730=AXIS2_PLACEMENT_3D ( 'NONE', #4300, #413, #763 ) ;
#1736=FACE_OUTER_BOUND ( 'NONE', #1546, .T. ) ;
#1737=CARTESIAN_POINT ( 'NONE',  ( 8.066546224052645542, -13.73374999999999524, 8.066546224052645542 ) ) ;
#1748=CARTESIAN_POINT ( 'NONE',  ( 17.78000050552179800, -17.78000000000000114, 17.78000050552179445 ) ) ;
#1750=AXIS2_PLACEMENT_3D ( 'NONE', #2936, #4047, #3323 ) ;
#1751=VECTOR ( 'NONE', #4413, 1000.000000000000000 ) ;
#1766=CARTESIAN_POINT ( 'NONE',  ( 3.040000505521796015, -17.78000000000000114, 3.040000505521795571 ) ) ;
#1776=DIRECTION ( 'NONE',  ( -1.000000000000000000, -0.000000000000000000, -0.000000000000000000 ) ) ;
#1778=ORIENTED_EDGE ( 'NONE', *, *, #381, .F. ) ;
#1783=SHAPE_DEFINITION_REPRESENTATION ( #3171, #2003 ) ;
#1784=ADVANCED_FACE ( 'NONE', ( #4220 ), #2352, .T. ) ;
#1787=LINE ( 'NONE', #1436, #918 ) ;
#1788=CARTESIAN_POINT ( 'NONE',  ( 17.28000050552179445, -2.539999999999999591, 3.040000505521795571 ) ) ;
#1795=ORIENTED_EDGE ( 'NONE', *, *, #3982, .F. ) ;
#1803=( NAMED_UNIT ( * ) SI_UNIT ( $, .STERADIAN. ) SOLID_ANGLE_UNIT ( ) );
#1809=CARTESIAN_POINT ( 'NONE',  ( 3.040000505521795571, -17.28000000000000114, 17.78000050552179445 ) ) ;
#1813=DIRECTION ( 'NONE',  ( -1.000000000000000000, 0.000000000000000000, 0.000000000000000000 ) ) ;
#1818=DIRECTION ( 'NONE',  ( 0.000000000000000000, 0.000000000000000000, -1.000000000000000000 ) ) ;
#1827=DIRECTION ( 'NONE',  ( 0.000000000000000000, 0.000000000000000000, -1.000000000000000000 ) ) ;
#1841=FACE_BOUND ( 'NONE', #3198, .T. ) ;
#1843=ORIENTED_EDGE ( 'NONE', *, *, #2206, .T. ) ;
#1846=VERTEX_POINT ( 'NONE', #3096 ) ;
#1852=DIRECTION ( 'NONE',  ( -1.000000000000000000, 0.000000000000000000, 0.000000000000000000 ) ) ;
#1856=CARTESIAN_POINT ( 'NONE',  ( 17.78000050552179800, -17.78000000000000114, 17.28000050552179445 ) ) ;
#1863=EDGE_LOOP ( 'NONE', ( #3027, #3157, #538, #1526 ) ) ;
#1873=CIRCLE ( 'NONE', #813, 3.573750000000000426 ) ;
#1875=EDGE_CURVE ( 'NONE', #3180, #1954, #979, .T. ) ;
#1880=CARTESIAN_POINT ( 'NONE',  ( 17.28000050552179800, -17.78000000000000114, 2.540000505521796015 ) ) ;
#1883=DIRECTION ( 'NONE',  ( 0.000000000000000000, 0.000000000000000000, -1.000000000000000000 ) ) ;
#1889=CARTESIAN_POINT ( 'NONE',  ( 3.040000505521796015, -3.039999999999999147, 3.040000505521795571 ) ) ;
#1891=AXIS2_PLACEMENT_3D ( 'NONE', #2685, #4123, #2262 ) ;
#1892=CARTESIAN_POINT ( 'NONE',  ( 10.16000050552179701, -6.586249999999999716, 10.16000050552179701 ) ) ;
#1904=CYLINDRICAL_SURFACE ( 'NONE', #3210, 3.573749999999999538 ) ;
#1905=ADVANCED_FACE ( 'NONE', ( #3142 ), #320, .T. ) ;
#1907=DIRECTION ( 'NONE',  ( 0.000000000000000000, 1.000000000000000000, 0.000000000000000000 ) ) ;
#1908=DIRECTION ( 'NONE',  ( 0.000000000000000000, 0.000000000000000000, -1.000000000000000000 ) ) ;
#1911=EDGE_LOOP ( 'NONE', ( #1265, #4334, #383, #1669 ) ) ;
#1928=( BOUNDED_CURVE ( )  B_SPLINE_CURVE ( 3, ( #4252, #4586, #4182, #1033 ),
 .UNSPECIFIED., .F., .F. ) 
 B_SPLINE_CURVE_WITH_KNOTS ( ( 4, 4 ),
 ( 1.570796326794896558, 3.141592653589793116 ),
 .UNSPECIFIED. ) 
 CURVE ( )  GEOMETRIC_REPRESENTATION_ITEM ( )  RATIONAL_B_SPLINE_CURVE ( ( 1.000000000000000000, 0.8047378541243649375, 0.8047378541243649375, 1.000000000000000000 ) ) 
 REPRESENTATION_ITEM ( '' )  );
#1931=AXIS2_PLACEMENT_3D ( 'NONE', #1371, #3172, #673 ) ;
#1936=ORIENTED_EDGE ( 'NONE', *, *, #4404, .F. ) ;
#1939=CARTESIAN_POINT ( 'NONE',  ( 17.28000050552179800, -17.28000000000000114, 3.040000505521795571 ) ) ;
#1948=DIRECTION ( 'NONE',  ( -0.000000000000000000, -0.000000000000000000, -1.000000000000000000 ) ) ;
#1954=VERTEX_POINT ( 'NONE', #4133 ) ;
#1955=FACE_OUTER_BOUND ( 'NONE', #2612, .T. ) ;
#1957=COLOUR_RGB ( '', 0.40784314, 0.44705882, 0.49803922) ;
#1963=CARTESIAN_POINT ( 'NONE',  ( 17.78000050552179445, -3.039999999999999591, 17.78000050552179445 ) ) ;
#1964=AXIS2_PLACEMENT_3D ( 'NONE', #1748, #3173, #4611 ) ;
#1966=EDGE_CURVE ( 'NONE', #4397, #975, #307, .T. ) ;
#1968=VECTOR ( 'NONE', #2812, 1000.000000000000000 ) ;
#1977=DIRECTION ( 'NONE',  ( 1.000000000000000000, -0.000000000000000000, -0.000000000000000000 ) ) ;
#1978=ORIENTED_EDGE ( 'NONE', *, *, #3883, .T. ) ;
#1983=ORIENTED_EDGE ( 'NONE', *, *, #4335, .F. ) ;
#1986=CYLINDRICAL_SURFACE ( 'NONE', #722, 3.573750000000000426 ) ;
#1988=CARTESIAN_POINT ( 'NONE',  ( 17.78000050552179445, -2.539999999999999591, 17.28000050552179445 ) ) ;
#1992=EDGE_CURVE ( 'NONE', #3326, #3048, #2311, .T. ) ;
#1993=PLANE ( 'NONE',  #2010 ) ;
#2000=ORIENTED_EDGE ( 'NONE', *, *, #4375, .T. ) ;
#2001=EDGE_CURVE ( 'NONE', #992, #975, #508, .T. ) ;
#2003=SHAPE_REPRESENTATION ( 'Part 133_Varsay\X2\0131\X0\lan', ( #4483 ), #2816 ) ;
#2010=AXIS2_PLACEMENT_3D ( 'NONE', #3426, #4128, #2061 ) ;
#2016=ORIENTED_EDGE ( 'NONE', *, *, #3793, .F. ) ;
#2020=AXIS2_PLACEMENT_3D ( 'NONE', #1306, #2251, #1658 ) ;
#2028=VECTOR ( 'NONE', #3476, 1000.000000000000000 ) ;
#2047=CARTESIAN_POINT ( 'NONE',  ( 2.540000505521796015, -17.78000000000000114, 3.040000505521795571 ) ) ;
#2048=ORIENTED_EDGE ( 'NONE', *, *, #2959, .T. ) ;
#2050=AXIS2_PLACEMENT_3D ( 'NONE', #2608, #4046, #844 ) ;
#2061=DIRECTION ( 'NONE',  ( -1.000000000000000000, 0.000000000000000000, -0.000000000000000000 ) ) ;
#2062=CIRCLE ( 'NONE', #2799, 0.5000000000000000000 ) ;
#2068=ADVANCED_BREP_SHAPE_REPRESENTATION ( '', ( #391, #4483 ), #2816 ) ;
#2069=LINE ( 'NONE', #2047, #3800 ) ;
#2073=ORIENTED_EDGE ( 'NONE', *, *, #3677, .F. ) ;
#2078=ORIENTED_EDGE ( 'NONE', *, *, #865, .T. ) ;
#2081=CARTESIAN_POINT ( 'NONE',  ( 13.73375050552179744, -10.16000000000000014, 6.586250505521794807 ) ) ;
#2083=DIRECTION ( 'NONE',  ( 0.000000000000000000, 0.000000000000000000, 1.000000000000000000 ) ) ;
#2084=CARTESIAN_POINT ( 'NONE',  ( 17.28000050552179800, -17.78000000000000114, 3.040000505521795571 ) ) ;
#2086=CARTESIAN_POINT ( 'NONE',  ( 2.540000505521795127, -17.28000000000000114, 2.540000505521796015 ) ) ;
#2089=DIRECTION ( 'NONE',  ( 0.000000000000000000, 0.000000000000000000, -1.000000000000000000 ) ) ;
#2093=CARTESIAN_POINT ( 'NONE',  ( 6.586250505521797471, -10.16000000000000014, 17.78000050552179445 ) ) ;
#2095=ORIENTED_EDGE ( 'NONE', *, *, #667, .F. ) ;
#2102=DIRECTION ( 'NONE',  ( -1.000000000000000000, 0.000000000000000000, 8.673617379884026597E-16 ) ) ;
#2123=FILL_AREA_STYLE ('',( #1405 ) ) ;
#2128=EDGE_CURVE ( 'NONE', #2747, #3571, #1267, .T. ) ;
#2130=AXIS2_PLACEMENT_3D ( 'NONE', #1426, #1776, #2505 ) ;
#2132=CARTESIAN_POINT ( 'NONE',  ( 17.78000050552179445, -10.16000000000000014, 10.16000050552179701 ) ) ;
#2135=EDGE_CURVE ( 'NONE', #4121, #1846, #1599, .T. ) ;
#2138=CARTESIAN_POINT ( 'NONE',  ( 3.040000505521796015, -3.039999999999999591, 17.78000050552179445 ) ) ;
#2141=ORIENTED_EDGE ( 'NONE', *, *, #1992, .T. ) ;
#2142=CARTESIAN_POINT ( 'NONE',  ( 10.16000050552179701, -10.16000000000000014, 2.540000505521796015 ) ) ;
#2155=AXIS2_PLACEMENT_3D ( 'NONE', #1135, #765, #3293 ) ;
#2163=AXIS2_PLACEMENT_3D ( 'NONE', #3029, #3788, #2703 ) ;
#2172=CIRCLE ( 'NONE', #4357, 0.5000000000000004441 ) ;
#2181=DIRECTION ( 'NONE',  ( 0.000000000000000000, 0.000000000000000000, -1.000000000000000000 ) ) ;
#2182=ORIENTED_EDGE ( 'NONE', *, *, #158, .T. ) ;
#2187=AXIS2_PLACEMENT_3D ( 'NONE', #1766, #294, #4628 ) ;
#2189=ORIENTED_EDGE ( 'NONE', *, *, #3783, .F. ) ;
#2191=EDGE_LOOP ( 'NONE', ( #214, #2719, #4191 ) ) ;
#2206=EDGE_CURVE ( 'NONE', #3396, #4255, #1156, .T. ) ;
#2216=ADVANCED_FACE ( 'NONE', ( #3287, #1271 ), #1993, .F. ) ;
#2222=LINE ( 'NONE', #1464, #2594 ) ;
#2225=LINE ( 'NONE', #1486, #2894 ) ;
#2229=CIRCLE ( 'NONE', #960, 3.573749999999999538 ) ;
#2230=SPHERICAL_SURFACE ( 'NONE', #232, 0.5000000000000000000 ) ;
#2235=AXIS2_PLACEMENT_3D ( 'NONE', #830, #374, #1818 ) ;
#2241=AXIS2_PLACEMENT_3D ( 'NONE', #1311, #585, #215 ) ;
#2243=DIRECTION ( 'NONE',  ( 0.000000000000000000, -1.000000000000000000, 0.000000000000000000 ) ) ;
#2245=VERTEX_POINT ( 'NONE', #3475 ) ;
#2249=DIRECTION ( 'NONE',  ( -1.000000000000000000, 0.000000000000000000, -0.000000000000000000 ) ) ;
#2251=DIRECTION ( 'NONE',  ( 0.000000000000000000, -1.000000000000000000, 0.000000000000000000 ) ) ;
#2262=DIRECTION ( 'NONE',  ( 0.000000000000000000, 0.000000000000000000, 1.000000000000000000 ) ) ;
#2267=ADVANCED_FACE ( 'NONE', ( #1694 ), #2712, .T. ) ;
#2279=EDGE_LOOP ( 'NONE', ( #1978, #1493, #2411, #133 ) ) ;
#2292=PLANE ( 'NONE',  #2020 ) ;
#2295=ORIENTED_EDGE ( 'NONE', *, *, #381, .T. ) ;
#2303=ADVANCED_FACE ( 'NONE', ( #2418 ), #3540, .T. ) ;
#2305=ADVANCED_FACE ( 'NONE', ( #1736 ), #3207, .T. ) ;
#2309=CARTESIAN_POINT ( 'NONE',  ( 17.28000050552179445, -3.039999999999999591, 17.78000050552179445 ) ) ;
#2311=LINE ( 'NONE', #2667, #386 ) ;
#2318=SPHERICAL_SURFACE ( 'NONE', #2163, 0.5000000000000000000 ) ;
#2319=CYLINDRICAL_SURFACE ( 'NONE', #4143, 3.573750000000000426 ) ;
#2331=CIRCLE ( 'NONE', #3836, 0.5000000000000000000 ) ;
#2332=ORIENTED_EDGE ( 'NONE', *, *, #3005, .F. ) ;
#2341=EDGE_LOOP ( 'NONE', ( #2000, #3463, #2980, #2388 ) ) ;
#2342=CYLINDRICAL_SURFACE ( 'NONE', #136, 0.5000000000000004441 ) ;
#2343=CIRCLE ( 'NONE', #2130, 0.5000000000000000000 ) ;
#2344=LINE ( 'NONE', #2093, #1193 ) ;
#2349=ORIENTED_EDGE ( 'NONE', *, *, #2409, .T. ) ;
#2350=CARTESIAN_POINT ( 'NONE',  ( 3.040000505521796015, -3.039999999999999591, 3.040000505521796015 ) ) ;
#2352=SPHERICAL_SURFACE ( 'NONE', #2385, 0.5000000000000000000 ) ;
#2359=VERTEX_POINT ( 'NONE', #3860 ) ;
#2360=DIRECTION ( 'NONE',  ( 1.000000000000000000, 0.000000000000000000, 0.000000000000000000 ) ) ;
#2370=CARTESIAN_POINT ( 'NONE',  ( 10.16000050552179701, -6.586249999999999716, 10.16000050552179701 ) ) ;
#2374=ADVANCED_FACE ( 'NONE', ( #3933 ), #1407, .T. ) ;
#2380=DIRECTION ( 'NONE',  ( -0.000000000000000000, -0.000000000000000000, -1.000000000000000000 ) ) ;
#2381=ORIENTED_EDGE ( 'NONE', *, *, #4354, .F. ) ;
#2382=FACE_OUTER_BOUND ( 'NONE', #896, .T. ) ;
#2385=AXIS2_PLACEMENT_3D ( 'NONE', #3519, #3797, #1324 ) ;
#2387=( BOUNDED_CURVE ( )  B_SPLINE_CURVE ( 3, ( #1562, #139, #869, #4403 ),
 .UNSPECIFIED., .F., .T. ) 
 B_SPLINE_CURVE_WITH_KNOTS ( ( 4, 4 ),
 ( 1.570796326794896558, 3.141592653589793116 ),
 .UNSPECIFIED. ) 
 CURVE ( )  GEOMETRIC_REPRESENTATION_ITEM ( )  RATIONAL_B_SPLINE_CURVE ( ( 1.000000000000000000, 0.8047378541243649375, 0.8047378541243649375, 1.000000000000000000 ) ) 
 REPRESENTATION_ITEM ( '' )  );
#2388=ORIENTED_EDGE ( 'NONE', *, *, #961, .T. ) ;
#2389=ORIENTED_EDGE ( 'NONE', *, *, #4619, .F. ) ;
#2393=CARTESIAN_POINT ( 'NONE',  ( 2.540000505521796015, -17.78000000000000114, 17.28000050552179445 ) ) ;
#2404=FACE_OUTER_BOUND ( 'NONE', #443, .T. ) ;
#2406=DIRECTION ( 'NONE',  ( -0.000000000000000000, -0.000000000000000000, -1.000000000000000000 ) ) ;
#2409=EDGE_CURVE ( 'NONE', #3774, #3954, #1712, .T. ) ;
#2411=ORIENTED_EDGE ( 'NONE', *, *, #456, .T. ) ;
#2416=EDGE_LOOP ( 'NONE', ( #3370, #1036, #4111, #927 ) ) ;
#2418=FACE_OUTER_BOUND ( 'NONE', #4618, .T. ) ;
#2427=DIRECTION ( 'NONE',  ( 0.000000000000000000, 0.000000000000000000, 1.000000000000000000 ) ) ;
#2432=EDGE_CURVE ( 'NONE', #4095, #3460, #2387, .T. ) ;
#2454=CARTESIAN_POINT ( 'NONE',  ( 17.78000050552179800, -17.78000000000000114, 3.040000505521795571 ) ) ;
#2476=DIRECTION ( 'NONE',  ( 1.707404996040164265E-16, -1.000000000000000000, 0.000000000000000000 ) ) ;
#2494=CYLINDRICAL_SURFACE ( 'NONE', #4450, 0.5000000000000000000 ) ;
#2498=DIRECTION ( 'NONE',  ( 0.000000000000000000, 0.000000000000000000, 1.000000000000000000 ) ) ;
#2499=CYLINDRICAL_SURFACE ( 'NONE', #1730, 3.573750000000000426 ) ;
#2505=DIRECTION ( 'NONE',  ( 0.000000000000000000, 0.000000000000000000, -1.000000000000000000 ) ) ;
#2508=ADVANCED_FACE ( 'NONE', ( #2950, #3311 ), #742, .T. ) ;
#2512=EDGE_LOOP ( 'NONE', ( #2073, #2868, #3151, #2381, #1200 ) ) ;
#2526=EDGE_LOOP ( 'NONE', ( #2638, #4163, #1936, #2189 ) ) ;
#2530=AXIS2_PLACEMENT_3D ( 'NONE', #186, #1907, #3340 ) ;
#2531=EDGE_CURVE ( 'NONE', #3559, #1846, #2225, .T. ) ;
#2533=AXIS2_PLACEMENT_3D ( 'NONE', #2803, #2102, #4289 ) ;
#2537=ORIENTED_EDGE ( 'NONE', *, *, #3080, .F. ) ;
#2542=ADVANCED_FACE ( 'NONE', ( #3661 ), #89, .T. ) ;
#2543=( BOUNDED_CURVE ( )  B_SPLINE_CURVE ( 3, ( #179, #4083, #432, #1224 ),
 .UNSPECIFIED., .F., .F. ) 
 B_SPLINE_CURVE_WITH_KNOTS ( ( 4, 4 ),
 ( 4.712388980384689674, 6.283185307179586232 ),
 .UNSPECIFIED. ) 
 CURVE ( )  GEOMETRIC_REPRESENTATION_ITEM ( )  RATIONAL_B_SPLINE_CURVE ( ( 1.000000000000000000, 0.8047378541243649375, 0.8047378541243649375, 1.000000000000000000 ) ) 
 REPRESENTATION_ITEM ( '' )  );
#2545=DIRECTION ( 'NONE',  ( 0.000000000000000000, 1.000000000000000000, 8.673617379884026597E-16 ) ) ;
#2550=ADVANCED_FACE ( 'NONE', ( #2881 ), #4348, .T. ) ;
#2555=CARTESIAN_POINT ( 'NONE',  ( 17.78000050552179800, -17.28000000000000114, 3.040000505521795571 ) ) ;
#2558=CIRCLE ( 'NONE', #1750, 0.5000000000000004441 ) ;
#2568=DIRECTION ( 'NONE',  ( -1.000000000000000000, 0.000000000000000000, 0.000000000000000000 ) ) ;
#2578=ORIENTED_EDGE ( 'NONE', *, *, #361, .T. ) ;
#2581=ADVANCED_FACE ( 'NONE', ( #786 ), #1904, .F. ) ;
#2583=DIRECTION ( 'NONE',  ( 0.000000000000000000, 0.000000000000000000, -1.000000000000000000 ) ) ;
#2586=DIRECTION ( 'NONE',  ( -1.000000000000000000, -0.000000000000000000, -0.000000000000000000 ) ) ;
#2587=CARTESIAN_POINT ( 'NONE',  ( 10.16000050552179701, -10.16000000000000014, 17.78000050552179445 ) ) ;
#2594=VECTOR ( 'NONE', #692, 1000.000000000000000 ) ;
#2596=DIRECTION ( 'NONE',  ( 0.000000000000000000, 0.000000000000000000, -1.000000000000000000 ) ) ;
#2599=AXIS2_PLACEMENT_3D ( 'NONE', #929, #3908, #2583 ) ;
#2608=CARTESIAN_POINT ( 'NONE',  ( 3.040000505521795571, -17.28000000000000114, 3.040000505521795571 ) ) ;
#2612=EDGE_LOOP ( 'NONE', ( #2820, #588, #330, #1138 ) ) ;
#2617=EDGE_LOOP ( 'NONE', ( #2911, #4643, #1795 ) ) ;
#2623=CARTESIAN_POINT ( 'NONE',  ( 13.73375050552179566, -12.25345428146915161, 13.73375050552179566 ) ) ;
#2631=CARTESIAN_POINT ( 'NONE',  ( 13.73375050552179744, -10.16000000000000014, 6.586250505521794807 ) ) ;
#2632=DIRECTION ( 'NONE',  ( -1.000000000000000000, 0.000000000000000000, 0.000000000000000000 ) ) ;
#2638=ORIENTED_EDGE ( 'NONE', *, *, #505, .T. ) ;
#2640=DIRECTION ( 'NONE',  ( 1.707404996040164265E-16, -1.000000000000000000, -0.000000000000000000 ) ) ;
#2641=AXIS2_PLACEMENT_3D ( 'NONE', #1594, #2243, #3330 ) ;
#2650=EDGE_LOOP ( 'NONE', ( #3162, #4460, #3342, #2655 ) ) ;
#2654=VECTOR ( 'NONE', #4066, 1000.000000000000000 ) ;
#2655=ORIENTED_EDGE ( 'NONE', *, *, #961, .F. ) ;
#2657=DIRECTION ( 'NONE',  ( -0.000000000000000000, -0.000000000000000000, -1.000000000000000000 ) ) ;
#2667=CARTESIAN_POINT ( 'NONE',  ( 3.040000505521795571, -17.78000000000000114, 17.78000050552179445 ) ) ;
#2678=EDGE_CURVE ( 'NONE', #1846, #245, #3756, .T. ) ;
#2681=DIRECTION ( 'NONE',  ( 0.000000000000000000, 0.000000000000000000, -1.000000000000000000 ) ) ;
#2685=CARTESIAN_POINT ( 'NONE',  ( 3.040000505521796015, -3.039999999999999591, 17.28000050552179445 ) ) ;
#2687=UNCERTAINTY_MEASURE_WITH_UNIT (LENGTH_MEASURE( 1.000000000000000082E-05 ), #3953, 'distance_accuracy_value', 'NONE');
#2697=EDGE_LOOP ( 'NONE', ( #3840, #402, #2078, #1178, #2987 ) ) ;
#2700=DIRECTION ( 'NONE',  ( 0.000000000000000000, 0.000000000000000000, -1.000000000000000000 ) ) ;
#2703=DIRECTION ( 'NONE',  ( 1.000000000000000000, 0.000000000000000000, 0.000000000000000000 ) ) ;
#2712=CYLINDRICAL_SURFACE ( 'NONE', #2599, 0.5000000000000004441 ) ;
#2713=CARTESIAN_POINT ( 'NONE',  ( 6.586250505521797471, -10.16000000000000014, 6.586250505521798360 ) ) ;
#2719=ORIENTED_EDGE ( 'NONE', *, *, #39, .T. ) ;
#2721=FACE_OUTER_BOUND ( 'NONE', #2526, .T. ) ;
#2723=ORIENTED_EDGE ( 'NONE', *, *, #3982, .T. ) ;
#2724=DIRECTION ( 'NONE',  ( 0.000000000000000000, 0.000000000000000000, -1.000000000000000000 ) ) ;
#2726=CARTESIAN_POINT ( 'NONE',  ( 2.540000505521796015, -10.16000000000000014, 6.586250505521796583 ) ) ;
#2727=EDGE_CURVE ( 'NONE', #4255, #4095, #3363, .T. ) ;
#2728=VERTEX_POINT ( 'NONE', #4406 ) ;
#2730=CARTESIAN_POINT ( 'NONE',  ( 13.73375050552179566, -8.066545718530848674, 6.586250505521797471 ) ) ;
#2731=ORIENTED_EDGE ( 'NONE', *, *, #2128, .F. ) ;
#2738=DIRECTION ( 'NONE',  ( -0.000000000000000000, 0.000000000000000000, -1.000000000000000000 ) ) ;
#2739=DIRECTION ( 'NONE',  ( 1.000000000000000000, 0.000000000000000000, 0.000000000000000000 ) ) ;
#2742=AXIS2_PLACEMENT_3D ( 'NONE', #4202, #4610, #1416 ) ;
#2747=VERTEX_POINT ( 'NONE', #1194 ) ;
#2749=CIRCLE ( 'NONE', #3361, 0.5000000000000004441 ) ;
#2750=CARTESIAN_POINT ( 'NONE',  ( 2.540000505521796015, -3.039999999999999147, 3.040000505521795571 ) ) ;
#2752=EDGE_CURVE ( 'NONE', #3396, #2359, #2229, .T. ) ;
#2753=ORIENTED_EDGE ( 'NONE', *, *, #51, .T. ) ;
#2757=CIRCLE ( 'NONE', #2530, 0.5000000000000004441 ) ;
#2762=CYLINDRICAL_SURFACE ( 'NONE', #1931, 3.573750000000000426 ) ;
#2764=LINE ( 'NONE', #1327, #468 ) ;
#2777=EDGE_CURVE ( 'NONE', #1450, #1649, #3394, .T. ) ;
#2785=ADVANCED_FACE ( 'NONE', ( #1642 ), #1986, .F. ) ;
#2789=DIRECTION ( 'NONE',  ( -0.000000000000000000, 1.000000000000000000, -0.000000000000000000 ) ) ;
#2790=ORIENTED_EDGE ( 'NONE', *, *, #3155, .F. ) ;
#2797=EDGE_CURVE ( 'NONE', #3571, #1713, #2749, .T. ) ;
#2799=AXIS2_PLACEMENT_3D ( 'NONE', #3587, #1128, #1053 ) ;
#2803=CARTESIAN_POINT ( 'NONE',  ( 3.040000505521795571, -17.28000000000000114, 17.28000050552179445 ) ) ;
#2812=DIRECTION ( 'NONE',  ( -1.000000000000000000, -0.000000000000000000, -0.000000000000000000 ) ) ;
#2813=VERTEX_POINT ( 'NONE', #2726 ) ;
#2814=ADVANCED_FACE ( 'NONE', ( #3156 ), #990, .T. ) ;
#2816=( GEOMETRIC_REPRESENTATION_CONTEXT ( 3 ) GLOBAL_UNCERTAINTY_ASSIGNED_CONTEXT ( ( #1622 ) ) GLOBAL_UNIT_ASSIGNED_CONTEXT ( ( #4035, #859, #458 ) ) REPRESENTATION_CONTEXT ( 'NONE', 'WORKASPACE' ) );
#2817=LINE ( 'NONE', #1039, #2654 ) ;
#2820=ORIENTED_EDGE ( 'NONE', *, *, #2531, .T. ) ;
#2822=( BOUNDED_CURVE ( )  B_SPLINE_CURVE ( 3, ( #1565, #2982, #1214, #2631 ),
 .UNSPECIFIED., .F., .T. ) 
 B_SPLINE_CURVE_WITH_KNOTS ( ( 4, 4 ),
 ( 4.712388980384689674, 6.283185307179586232 ),
 .UNSPECIFIED. ) 
 CURVE ( )  GEOMETRIC_REPRESENTATION_ITEM ( )  RATIONAL_B_SPLINE_CURVE ( ( 1.000000000000000000, 0.8047378541243649375, 0.8047378541243649375, 1.000000000000000000 ) ) 
 REPRESENTATION_ITEM ( '' )  );
#2827=CARTESIAN_POINT ( 'NONE',  ( 17.28000050552179445, -2.539999999999996927, 17.28000050552179445 ) ) ;
#2839=CARTESIAN_POINT ( 'NONE',  ( 17.28000050552179800, -17.28000000000000114, 17.28000050552179445 ) ) ;
#2847=ORIENTED_EDGE ( 'NONE', *, *, #3740, .F. ) ;
#2856=DIRECTION ( 'NONE',  ( -1.000000000000000000, 0.000000000000000000, 0.000000000000000000 ) ) ;
#2857=VERTEX_POINT ( 'NONE', #4525 ) ;
#2863=ORIENTED_EDGE ( 'NONE', *, *, #2678, .F. ) ;
#2864=EDGE_LOOP ( 'NONE', ( #2349, #4000, #3186 ) ) ;
#2866=EDGE_CURVE ( 'NONE', #566, #2857, #2344, .T. ) ;
#2868=ORIENTED_EDGE ( 'NONE', *, *, #712, .T. ) ;
#2869=LINE ( 'NONE', #4597, #3369 ) ;
#2881=FACE_OUTER_BOUND ( 'NONE', #2650, .T. ) ;
#2884=FACE_OUTER_BOUND ( 'NONE', #2864, .T. ) ;
#2886=ORIENTED_EDGE ( 'NONE', *, *, #2962, .T. ) ;
#2894=VECTOR ( 'NONE', #3994, 1000.000000000000000 ) ;
#2902=CARTESIAN_POINT ( 'NONE',  ( 17.28000050552179800, -17.28000000000000114, 3.040000505521796015 ) ) ;
#2905=CARTESIAN_POINT ( 'NONE',  ( 13.73375050552179744, -10.16000000000000014, 2.540000505521796015 ) ) ;
#2911=ORIENTED_EDGE ( 'NONE', *, *, #2797, .F. ) ;
#2917=AXIS2_PLACEMENT_3D ( 'NONE', #1544, #4452, #4071 ) ;
#2936=CARTESIAN_POINT ( 'NONE',  ( 3.040000505521796015, -17.28000000000000114, 3.040000505521796015 ) ) ;
#2938=ORIENTED_EDGE ( 'NONE', *, *, #344, .T. ) ;
#2945=FACE_OUTER_BOUND ( 'NONE', #4027, .T. ) ;
#2947=FACE_OUTER_BOUND ( 'NONE', #635, .T. ) ;
#2950=FACE_OUTER_BOUND ( 'NONE', #1572, .T. ) ;
#2959=EDGE_CURVE ( 'NONE', #4067, #3954, #3201, .T. ) ;
#2962=EDGE_CURVE ( 'NONE', #3180, #3625, #2343, .T. ) ;
#2972=DIRECTION ( 'NONE',  ( -0.000000000000000000, -0.000000000000000000, 1.000000000000000000 ) ) ;
#2974=AXIS2_PLACEMENT_3D ( 'NONE', #1183, #2181, #2249 ) ;
#2980=ORIENTED_EDGE ( 'NONE', *, *, #3586, .T. ) ;
#2982=CARTESIAN_POINT ( 'NONE',  ( 12.25345478699094670, -13.73374999999999524, 8.066546224052645542 ) ) ;
#2987=ORIENTED_EDGE ( 'NONE', *, *, #2206, .F. ) ;
#2992=CARTESIAN_POINT ( 'NONE',  ( 13.73375050552179744, -10.16000000000000014, 13.73375050552179744 ) ) ;
#2999=ADVANCED_FACE ( 'NONE', ( #2884 ), #377, .T. ) ;
#3005=EDGE_CURVE ( 'NONE', #4397, #1450, #3555, .T. ) ;
#3016=CARTESIAN_POINT ( 'NONE',  ( 17.78000050552179800, -17.28000000000000114, 3.040000505521795571 ) ) ;
#3022=ORIENTED_EDGE ( 'NONE', *, *, #3357, .T. ) ;
#3027=ORIENTED_EDGE ( 'NONE', *, *, #1966, .F. ) ;
#3029=CARTESIAN_POINT ( 'NONE',  ( 3.040000505521796015, -17.28000000000000114, 17.28000050552179445 ) ) ;
#3043=CARTESIAN_POINT ( 'NONE',  ( 13.73375050552179744, -10.16000000000000014, 13.73375050552179744 ) ) ;
#3047=AXIS2_PLACEMENT_3D ( 'NONE', #4299, #3307, #85 ) ;
#3048=VERTEX_POINT ( 'NONE', #3223 ) ;
#3052=CARTESIAN_POINT ( 'NONE',  ( 2.540000505521796015, -17.78000000000000114, 17.78000050552179445 ) ) ;
#3054=ORIENTED_EDGE ( 'NONE', *, *, #2727, .T. ) ;
#3058=DIRECTION ( 'NONE',  ( 0.000000000000000000, 0.000000000000000000, -1.000000000000000000 ) ) ;
#3061=CIRCLE ( 'NONE', #1038, 0.5000000000000004441 ) ;
#3063=LINE ( 'NONE', #4193, #770 ) ;
#3070=CARTESIAN_POINT ( 'NONE',  ( 10.16000050552179701, -10.16000000000000014, 17.78000050552179445 ) ) ;
#3080=EDGE_CURVE ( 'NONE', #1649, #4121, #2817, .T. ) ;
#3082=CARTESIAN_POINT ( 'NONE',  ( 17.28000050552179445, -2.539999999999999591, 17.78000050552179445 ) ) ;
#3089=VECTOR ( 'NONE', #3288, 1000.000000000000000 ) ;
#3095=CARTESIAN_POINT ( 'NONE',  ( 12.25345478699094670, -13.73374999999999524, 12.25345478699094670 ) ) ;
#3096=CARTESIAN_POINT ( 'NONE',  ( 3.040000505521796015, -2.539999999999999591, 17.28000050552179445 ) ) ;
#3110=DIRECTION ( 'NONE',  ( -0.000000000000000000, -0.000000000000000000, -1.000000000000000000 ) ) ;
#3111=EDGE_LOOP ( 'NONE', ( #1163, #3556, #282, #2731 ) ) ;
#3118=CARTESIAN_POINT ( 'NONE',  ( 3.040000505521796015, -2.539999999999999591, 3.040000505521795571 ) ) ;
#3121=CARTESIAN_POINT ( 'NONE',  ( 2.540000505521796015, -17.28000000000000114, 17.28000050552179445 ) ) ;
#3142=FACE_OUTER_BOUND ( 'NONE', #2279, .T. ) ;
#3146=PLANE ( 'NONE',  #1964 ) ;
#3151=ORIENTED_EDGE ( 'NONE', *, *, #4603, .T. ) ;
#3154=AXIS2_PLACEMENT_3D ( 'NONE', #2142, #3626, #3255 ) ;
#3155=EDGE_CURVE ( 'NONE', #3954, #4040, #1471, .T. ) ;
#3156=FACE_OUTER_BOUND ( 'NONE', #1863, .T. ) ;
#3157=ORIENTED_EDGE ( 'NONE', *, *, #3500, .F. ) ;
#3158=ORIENTED_EDGE ( 'NONE', *, *, #1875, .F. ) ;
#3159=VECTOR ( 'NONE', #1373, 1000.000000000000000 ) ;
#3162=ORIENTED_EDGE ( 'NONE', *, *, #3298, .T. ) ;
#3164=CARTESIAN_POINT ( 'NONE',  ( 10.16000050552179701, -13.73374999999999879, 10.16000050552179701 ) ) ;
#3169=EDGE_CURVE ( 'NONE', #3326, #975, #2062, .T. ) ;
#3171=PRODUCT_DEFINITION_SHAPE ( 'NONE', 'NONE',  #1640 ) ;
#3172=DIRECTION ( 'NONE',  ( -1.000000000000000000, -0.000000000000000000, -0.000000000000000000 ) ) ;
#3173=DIRECTION ( 'NONE',  ( 0.000000000000000000, 1.000000000000000000, -0.000000000000000000 ) ) ;
#3180=VERTEX_POINT ( 'NONE', #3893 ) ;
#3186=ORIENTED_EDGE ( 'NONE', *, *, #505, .F. ) ;
#3198=EDGE_LOOP ( 'NONE', ( #1609, #850 ) ) ;
#3201=LINE ( 'NONE', #4280, #4009 ) ;
#3205=AXIS2_PLACEMENT_3D ( 'NONE', #4648, #1431, #3229 ) ;
#3207=SPHERICAL_SURFACE ( 'NONE', #3205, 0.5000000000000000000 ) ;
#3210=AXIS2_PLACEMENT_3D ( 'NONE', #109, #4234, #1011 ) ;
#3214=CARTESIAN_POINT ( 'NONE',  ( 17.28000050552179445, -3.039999999999999591, 3.040000505521795571 ) ) ;
#3219=CARTESIAN_POINT ( 'NONE',  ( 17.78000050552179445, -10.16000000000000014, 10.16000050552179701 ) ) ;
#3220=ORIENTED_EDGE ( 'NONE', *, *, #3740, .T. ) ;
#3223=CARTESIAN_POINT ( 'NONE',  ( 3.040000505521795571, -17.78000000000000114, 3.040000505521795571 ) ) ;
#3229=DIRECTION ( 'NONE',  ( 1.000000000000000000, 0.000000000000000000, 0.000000000000000000 ) ) ;
#3237=FACE_OUTER_BOUND ( 'NONE', #2191, .T. ) ;
#3246=CARTESIAN_POINT ( 'NONE',  ( 10.16000050552179701, -6.586249999999999716, 10.16000050552179701 ) ) ;
#3247=CIRCLE ( 'NONE', #2050, 0.5000000000000000000 ) ;
#3255=DIRECTION ( 'NONE',  ( -1.000000000000000000, 0.000000000000000000, 0.000000000000000000 ) ) ;
#3261=DIRECTION ( 'NONE',  ( -1.000000000000000000, 0.000000000000000000, 0.000000000000000000 ) ) ;
#3264=DIRECTION ( 'NONE',  ( 0.000000000000000000, 0.000000000000000000, 1.000000000000000000 ) ) ;
#3265=CARTESIAN_POINT ( 'NONE',  ( 3.040000505521796015, -3.039999999999999147, 17.28000050552179445 ) ) ;
#3276=ORIENTED_EDGE ( 'NONE', *, *, #2135, .F. ) ;
#3283=VECTOR ( 'NONE', #1948, 1000.000000000000000 ) ;
#3287=FACE_OUTER_BOUND ( 'NONE', #2416, .T. ) ;
#3288=DIRECTION ( 'NONE',  ( -1.000000000000000000, -0.000000000000000000, -0.000000000000000000 ) ) ;
#3293=DIRECTION ( 'NONE',  ( -1.000000000000000000, 0.000000000000000000, 0.000000000000000000 ) ) ;
#3295=CARTESIAN_POINT ( 'NONE',  ( 17.78000050552179445, -2.539999999999999591, 17.78000050552179445 ) ) ;
#3298=EDGE_CURVE ( 'NONE', #2245, #1846, #2331, .T. ) ;
#3299=VECTOR ( 'NONE', #619, 1000.000000000000000 ) ;
#3307=DIRECTION ( 'NONE',  ( -1.000000000000000000, 0.000000000000000000, 0.000000000000000000 ) ) ;
#3309=DIRECTION ( 'NONE',  ( 1.000000000000000000, 0.000000000000000000, 0.000000000000000000 ) ) ;
#3311=FACE_BOUND ( 'NONE', #355, .T. ) ;
#3313=CARTESIAN_POINT ( 'NONE',  ( 17.28000050552179445, -3.039999999999999591, 2.540000505521796015 ) ) ;
#3323=DIRECTION ( 'NONE',  ( -8.673617379884027583E-16, -1.000000000000000000, 0.000000000000000000 ) ) ;
#3326=VERTEX_POINT ( 'NONE', #1701 ) ;
#3330=DIRECTION ( 'NONE',  ( 0.000000000000000000, 0.000000000000000000, -1.000000000000000000 ) ) ;
#3331=ORIENTED_EDGE ( 'NONE', *, *, #467, .T. ) ;
#3340=DIRECTION ( 'NONE',  ( 0.000000000000000000, 0.000000000000000000, 1.000000000000000000 ) ) ;
#3342=ORIENTED_EDGE ( 'NONE', *, *, #424, .F. ) ;
#3344=DIRECTION ( 'NONE',  ( -0.000000000000000000, -0.000000000000000000, 1.000000000000000000 ) ) ;
#3346=ORIENTED_EDGE ( 'NONE', *, *, #1966, .T. ) ;
#3347=EDGE_LOOP ( 'NONE', ( #2790, #4360, #3628, #3955 ) ) ;
#3357=EDGE_CURVE ( 'NONE', #1713, #3326, #3612, .T. ) ;
#3359=ORIENTED_EDGE ( 'NONE', *, *, #2432, .F. ) ;
#3361=AXIS2_PLACEMENT_3D ( 'NONE', #1313, #945, #1012 ) ;
#3363=( BOUNDED_CURVE ( )  B_SPLINE_CURVE ( 3, ( #4048, #4477, #3717, #1892 ),
 .UNSPECIFIED., .F., .F. ) 
 B_SPLINE_CURVE_WITH_KNOTS ( ( 4, 4 ),
 ( 3.141592653589793116, 4.712388980384689674 ),
 .UNSPECIFIED. ) 
 CURVE ( )  GEOMETRIC_REPRESENTATION_ITEM ( )  RATIONAL_B_SPLINE_CURVE ( ( 1.000000000000000000, 0.8047378541243649375, 0.8047378541243649375, 1.000000000000000000 ) ) 
 REPRESENTATION_ITEM ( '' )  );
#3369=VECTOR ( 'NONE', #4267, 1000.000000000000000 ) ;
#3370=ORIENTED_EDGE ( 'NONE', *, *, #3080, .T. ) ;
#3377=CIRCLE ( 'NONE', #533, 3.573750000000000426 ) ;
#3394=LINE ( 'NONE', #1615, #3583 ) ;
#3396=VERTEX_POINT ( 'NONE', #343 ) ;
#3401=CARTESIAN_POINT ( 'NONE',  ( 17.28000050552179445, -2.539999999999999591, 17.28000050552179445 ) ) ;
#3402=EDGE_CURVE ( 'NONE', #21, #4040, #1787, .T. ) ;
#3419=CARTESIAN_POINT ( 'NONE',  ( 17.78000050552179445, -10.16000000000000014, 10.16000050552179701 ) ) ;
#3424=EDGE_CURVE ( 'NONE', #2245, #4121, #607, .T. ) ;
#3426=CARTESIAN_POINT ( 'NONE',  ( 2.540000505521796015, -2.539999999999999591, 17.78000050552179445 ) ) ;
#3435=ORIENTED_EDGE ( 'NONE', *, *, #2752, .F. ) ;
#3446=CIRCLE ( 'NONE', #2235, 0.5000000000000000000 ) ;
#3448=EDGE_CURVE ( 'NONE', #4095, #566, #2543, .T. ) ;
#3456=CARTESIAN_POINT ( 'NONE',  ( 10.16000050552179701, -13.73374999999999879, 10.16000050552179701 ) ) ;
#3460=VERTEX_POINT ( 'NONE', #2992 ) ;
#3463=ORIENTED_EDGE ( 'NONE', *, *, #2001, .T. ) ;
#3475=CARTESIAN_POINT ( 'NONE',  ( 2.540000505521796015, -3.039999999999999147, 17.28000050552179445 ) ) ;
#3476=DIRECTION ( 'NONE',  ( 0.000000000000000000, 0.000000000000000000, -1.000000000000000000 ) ) ;
#3484=DIRECTION ( 'NONE',  ( -1.000000000000000000, 0.000000000000000000, 0.000000000000000000 ) ) ;
#3493=ORIENTED_EDGE ( 'NONE', *, *, #1449, .T. ) ;
#3494=EDGE_LOOP ( 'NONE', ( #3580, #3346, #110 ) ) ;
#3495=CARTESIAN_POINT ( 'NONE',  ( 12.25345478699094670, -6.586249999999999716, 8.066546224052645542 ) ) ;
#3496=VERTEX_POINT ( 'NONE', #1624 ) ;
#3500=EDGE_CURVE ( 'NONE', #4121, #4397, #1550, .T. ) ;
#3505=CARTESIAN_POINT ( 'NONE',  ( 13.73375050552179744, -10.16000000000000014, 17.78000050552179445 ) ) ;
#3511=EDGE_LOOP ( 'NONE', ( #2048, #1616, #3757, #4538 ) ) ;
#3516=CARTESIAN_POINT ( 'NONE',  ( 17.78000050552179800, -17.28000000000000114, 17.78000050552179445 ) ) ;
#3518=ADVANCED_FACE ( 'NONE', ( #481 ), #223, .T. ) ;
#3519=CARTESIAN_POINT ( 'NONE',  ( 17.28000050552179445, -3.039999999999999591, 17.28000050552179445 ) ) ;
#3532=MECHANICAL_DESIGN_GEOMETRIC_PRESENTATION_REPRESENTATION('',(#1581),#295);
#3536=DIRECTION ( 'NONE',  ( -0.000000000000000000, 0.000000000000000000, 1.000000000000000000 ) ) ;
#3540=CYLINDRICAL_SURFACE ( 'NONE', #3807, 0.5000000000000004441 ) ;
#3547=AXIS2_PLACEMENT_3D ( 'NONE', #3265, #2545, #37 ) ;
#3552=CARTESIAN_POINT ( 'NONE',  ( 3.040000505521796015, -2.540000000000000480, 2.540000505521796015 ) ) ;
#3555=LINE ( 'NONE', #4259, #332 ) ;
#3556=ORIENTED_EDGE ( 'NONE', *, *, #2777, .F. ) ;
#3559=VERTEX_POINT ( 'NONE', #3118 ) ;
#3562=CARTESIAN_POINT ( 'NONE',  ( 17.78000050552179445, -10.16000000000000014, 6.586250505521796583 ) ) ;
#3571=VERTEX_POINT ( 'NONE', #976 ) ;
#3578=SURFACE_STYLE_FILL_AREA ( #2123 ) ;
#3580=ORIENTED_EDGE ( 'NONE', *, *, #3741, .T. ) ;
#3583=VECTOR ( 'NONE', #4120, 1000.000000000000000 ) ;
#3586=EDGE_CURVE ( 'NONE', #975, #2245, #268, .T. ) ;
#3587=CARTESIAN_POINT ( 'NONE',  ( 3.040000505521796015, -17.28000000000000114, 17.28000050552179445 ) ) ;
#3592=CARTESIAN_POINT ( 'NONE',  ( 17.28000050552179800, -17.28000000000000114, 17.28000050552179445 ) ) ;
#3593=EDGE_CURVE ( 'NONE', #3571, #4067, #3841, .T. ) ;
#3612=LINE ( 'NONE', #1856, #3089 ) ;
#3615=DIRECTION ( 'NONE',  ( -1.000000000000000000, 0.000000000000000000, 0.000000000000000000 ) ) ;
#3618=VECTOR ( 'NONE', #2640, 1000.000000000000000 ) ;
#3625=VERTEX_POINT ( 'NONE', #2084 ) ;
#3626=DIRECTION ( 'NONE',  ( 0.000000000000000000, 0.000000000000000000, -1.000000000000000000 ) ) ;
#3628=ORIENTED_EDGE ( 'NONE', *, *, #4084, .F. ) ;
#3639=ORIENTED_EDGE ( 'NONE', *, *, #4354, .T. ) ;
#3645=ORIENTED_EDGE ( 'NONE', *, *, #712, .F. ) ;
#3647=CLOSED_SHELL ( 'NONE', ( #4435, #2785, #32, #4423, #2581, #1230, #1383, #4110, #4184, #2216, #2508, #1595, #1517, #573, #2374, #1784, #784, #3735, #2303, #2814, #2267, #3820, #4496, #2999, #2305, #3839, #2542, #1255, #2550, #90, #4644, #3518, #1013, #1905 ) ) ;
#3648=AXIS2_PLACEMENT_3D ( 'NONE', #3016, #4462, #531 ) ;
#3652=AXIS2_PLACEMENT_3D ( 'NONE', #2827, #444, #706 ) ;
#3661=FACE_OUTER_BOUND ( 'NONE', #707, .T. ) ;
#3667=EDGE_LOOP ( 'NONE', ( #1568, #3435, #1843, #3054, #196 ) ) ;
#3673=ORIENTED_EDGE ( 'NONE', *, *, #1333, .F. ) ;
#3677=EDGE_CURVE ( 'NONE', #566, #1305, #71, .T. ) ;
#3679=CYLINDRICAL_SURFACE ( 'NONE', #3648, 0.5000000000000000000 ) ;
#3680=FACE_OUTER_BOUND ( 'NONE', #3667, .T. ) ;
#3704=DIRECTION ( 'NONE',  ( 1.000000000000000000, 0.000000000000000000, 0.000000000000000000 ) ) ;
#3717=CARTESIAN_POINT ( 'NONE',  ( 8.066546224052645542, -6.586249999999999716, 12.25345478699094670 ) ) ;
#3722=DIRECTION ( 'NONE',  ( -1.000000000000000000, 0.000000000000000000, 0.000000000000000000 ) ) ;
#3735=ADVANCED_FACE ( 'NONE', ( #1409 ), #1387, .T. ) ;
#3740=EDGE_CURVE ( 'NONE', #1351, #2813, #1873, .T. ) ;
#3741=EDGE_CURVE ( 'NONE', #3326, #4397, #4347, .T. ) ;
#3742=LINE ( 'NONE', #1963, #1146 ) ;
#3744=ORIENTED_EDGE ( 'NONE', *, *, #2752, .T. ) ;
#3752=CARTESIAN_POINT ( 'NONE',  ( 0.000000000000000000, 0.000000000000000000, 0.000000000000000000 ) ) ;
#3756=LINE ( 'NONE', #536, #1647 ) ;
#3757=ORIENTED_EDGE ( 'NONE', *, *, #2128, .T. ) ;
#3760=FACE_BOUND ( 'NONE', #382, .T. ) ;
#3770=ORIENTED_EDGE ( 'NONE', *, *, #3741, .F. ) ;
#3774=VERTEX_POINT ( 'NONE', #1048 ) ;
#3783=EDGE_CURVE ( 'NONE', #3774, #3559, #2869, .T. ) ;
#3788=DIRECTION ( 'NONE',  ( 0.000000000000000000, 1.000000000000000000, 0.000000000000000000 ) ) ;
#3793=EDGE_CURVE ( 'NONE', #3496, #4402, #1433, .T. ) ;
#3797=DIRECTION ( 'NONE',  ( -0.000000000000000000, 1.000000000000000000, 0.000000000000000000 ) ) ;
#3800=VECTOR ( 'NONE', #4631, 1000.000000000000000 ) ;
#3806=DIRECTION ( 'NONE',  ( 0.000000000000000000, 0.000000000000000000, -1.000000000000000000 ) ) ;
#3807=AXIS2_PLACEMENT_3D ( 'NONE', #1169, #4265, #2083 ) ;
#3810=FACE_OUTER_BOUND ( 'NONE', #3494, .T. ) ;
#3813=ORIENTED_EDGE ( 'NONE', *, *, #1354, .T. ) ;
#3820=ADVANCED_FACE ( 'NONE', ( #1611 ), #2342, .T. ) ;
#3825=AXIS2_PLACEMENT_3D ( 'NONE', #3070, #1203, #1602 ) ;
#3836=AXIS2_PLACEMENT_3D ( 'NONE', #3894, #2738, #1343 ) ;
#3839=ADVANCED_FACE ( 'NONE', ( #3810 ), #2318, .T. ) ;
#3840=ORIENTED_EDGE ( 'NONE', *, *, #158, .F. ) ;
#3841=LINE ( 'NONE', #3516, #2028 ) ;
#3846=CARTESIAN_POINT ( 'NONE',  ( 13.73375050552179744, -10.16000000000000014, 6.586250505521794807 ) ) ;
#3860=CARTESIAN_POINT ( 'NONE',  ( 13.73375050552179744, -10.16000000000000014, 17.78000050552179445 ) ) ;
#3871=LINE ( 'NONE', #3897, #1968 ) ;
#3876=PRODUCT ( 'Part 133_Varsay\X2\0131\X0\lan', 'Part 133_Varsay\X2\0131\X0\lan', '', ( #778 ) ) ;
#3881=ORIENTED_EDGE ( 'NONE', *, *, #3448, .T. ) ;
#3883=EDGE_CURVE ( 'NONE', #356, #21, #732, .T. ) ;
#3888=CARTESIAN_POINT ( 'NONE',  ( 17.28000050552179445, -3.039999999999999591, 17.78000050552179445 ) ) ;
#3890=CARTESIAN_POINT ( 'NONE',  ( 2.540000505521796015, -17.28000000000000114, 3.040000505521795571 ) ) ;
#3893=CARTESIAN_POINT ( 'NONE',  ( 17.28000050552179800, -17.28000000000000114, 2.540000505521796015 ) ) ;
#3894=CARTESIAN_POINT ( 'NONE',  ( 3.040000505521796015, -3.039999999999999591, 17.28000050552179445 ) ) ;
#3897=CARTESIAN_POINT ( 'NONE',  ( 17.78000050552179445, -10.16000000000000014, 6.586250505521796583 ) ) ;
#3902=EDGE_CURVE ( 'NONE', #245, #3774, #1175, .T. ) ;
#3908=DIRECTION ( 'NONE',  ( 1.000000000000000000, 0.000000000000000000, 0.000000000000000000 ) ) ;
#3919=LINE ( 'NONE', #3505, #1368 ) ;
#3933=FACE_OUTER_BOUND ( 'NONE', #3111, .T. ) ;
#3941=FACE_OUTER_BOUND ( 'NONE', #3347, .T. ) ;
#3953=( LENGTH_UNIT ( ) NAMED_UNIT ( * ) SI_UNIT ( .MILLI., .METRE. ) );
#3954=VERTEX_POINT ( 'NONE', #1423 ) ;
#3955=ORIENTED_EDGE ( 'NONE', *, *, #1449, .F. ) ;
#3958=AXIS2_PLACEMENT_3D ( 'NONE', #612, #4568, #3058 ) ;
#3982=EDGE_CURVE ( 'NONE', #1713, #1450, #3061, .T. ) ;
#3983=AXIS2_PLACEMENT_3D ( 'NONE', #1721, #4227, #2089 ) ;
#3987=FACE_OUTER_BOUND ( 'NONE', #1288, .T. ) ;
#3989=APPLICATION_CONTEXT ( 'automotive_design' ) ;
#3994=DIRECTION ( 'NONE',  ( -0.000000000000000000, -0.000000000000000000, 1.000000000000000000 ) ) ;
#4000=ORIENTED_EDGE ( 'NONE', *, *, #3155, .T. ) ;
#4009=VECTOR ( 'NONE', #1473, 1000.000000000000000 ) ;
#4024=DIRECTION ( 'NONE',  ( 0.000000000000000000, 0.000000000000000000, 1.000000000000000000 ) ) ;
#4027=EDGE_LOOP ( 'NONE', ( #2886, #3673, #653, #3158 ) ) ;
#4035=( LENGTH_UNIT ( ) NAMED_UNIT ( * ) SI_UNIT ( .MILLI., .METRE. ) );
#4040=VERTEX_POINT ( 'NONE', #3313 ) ;
#4041=FACE_OUTER_BOUND ( 'NONE', #3511, .T. ) ;
#4044=ORIENTED_EDGE ( 'NONE', *, *, #3677, .T. ) ;
#4045=CARTESIAN_POINT ( 'NONE',  ( 17.28000050552179445, -3.039999999999999591, 3.040000505521795571 ) ) ;
#4046=DIRECTION ( 'NONE',  ( -0.000000000000000000, -0.000000000000000000, -1.000000000000000000 ) ) ;
#4047=DIRECTION ( 'NONE',  ( -1.000000000000000000, 8.673617379884026597E-16, 0.000000000000000000 ) ) ;
#4048=CARTESIAN_POINT ( 'NONE',  ( 6.586250505521797471, -10.16000000000000014, 13.73375050552179744 ) ) ;
#4051=EDGE_LOOP ( 'NONE', ( #1659, #2938, #3881, #172, #4377 ) ) ;
#4055=CARTESIAN_POINT ( 'NONE',  ( 10.16000050552179701, -10.16000000000000014, 17.78000050552179445 ) ) ;
#4066=DIRECTION ( 'NONE',  ( -1.000000000000000000, 0.000000000000000000, 0.000000000000000000 ) ) ;
#4067=VERTEX_POINT ( 'NONE', #2555 ) ;
#4071=DIRECTION ( 'NONE',  ( 0.000000000000000000, 0.000000000000000000, -1.000000000000000000 ) ) ;
#4083=CARTESIAN_POINT ( 'NONE',  ( 8.066546224052645542, -6.586249999999999716, 8.066546224052645542 ) ) ;
#4084=EDGE_CURVE ( 'NONE', #3180, #4067, #3446, .T. ) ;
#4088=AXIS2_PLACEMENT_3D ( 'NONE', #3214, #1101, #3264 ) ;
#4095=VERTEX_POINT ( 'NONE', #3246 ) ;
#4097=CARTESIAN_POINT ( 'NONE',  ( 3.040000505521796015, -3.039999999999999591, 2.540000505521796015 ) ) ;
#4103=ORIENTED_EDGE ( 'NONE', *, *, #3424, .T. ) ;
#4108=DIRECTION ( 'NONE',  ( 0.000000000000000000, -0.000000000000000000, -1.000000000000000000 ) ) ;
#4110=ADVANCED_FACE ( 'NONE', ( #4041, #1841 ), #1442, .F. ) ;
#4111=ORIENTED_EDGE ( 'NONE', *, *, #3005, .T. ) ;
#4118=FACE_OUTER_BOUND ( 'NONE', #4564, .T. ) ;
#4119=AXIS2_PLACEMENT_3D ( 'NONE', #3888, #1827, #3261 ) ;
#4120=DIRECTION ( 'NONE',  ( -1.707404996040164265E-16, 1.000000000000000000, 0.000000000000000000 ) ) ;
#4121=VERTEX_POINT ( 'NONE', #2138 ) ;
#4123=DIRECTION ( 'NONE',  ( -1.000000000000000000, 0.000000000000000000, 0.000000000000000000 ) ) ;
#4128=DIRECTION ( 'NONE',  ( 0.000000000000000000, 0.000000000000000000, -1.000000000000000000 ) ) ;
#4130=AXIS2_PLACEMENT_3D ( 'NONE', #1889, #519, #2632 ) ;
#4133=CARTESIAN_POINT ( 'NONE',  ( 3.040000505521796015, -17.28000000000000114, 2.540000505521796015 ) ) ;
#4138=VECTOR ( 'NONE', #1390, 1000.000000000000000 ) ;
#4141=AXIS2_PLACEMENT_3D ( 'NONE', #4441, #4158, #1252 ) ;
#4143=AXIS2_PLACEMENT_3D ( 'NONE', #423, #2586, #4024 ) ;
#4158=DIRECTION ( 'NONE',  ( 0.000000000000000000, -1.000000000000000000, 0.000000000000000000 ) ) ;
#4163=ORIENTED_EDGE ( 'NONE', *, *, #3402, .F. ) ;
#4164=CYLINDRICAL_SURFACE ( 'NONE', #4528, 0.5000000000000000000 ) ;
#4168=EDGE_CURVE ( 'NONE', #1649, #2747, #2757, .T. ) ;
#4182=CARTESIAN_POINT ( 'NONE',  ( 6.586250505521797471, -12.25345428146915161, 13.73375050552179566 ) ) ;
#4184=ADVANCED_FACE ( 'NONE', ( #1955 ), #2292, .F. ) ;
#4190=ORIENTED_EDGE ( 'NONE', *, *, #3169, .T. ) ;
#4191=ORIENTED_EDGE ( 'NONE', *, *, #456, .F. ) ;
#4193=CARTESIAN_POINT ( 'NONE',  ( 17.28000050552179800, -17.78000000000000114, 17.78000050552179445 ) ) ;
#4200=CIRCLE ( 'NONE', #2917, 0.5000000000000000000 ) ;
#4202=CARTESIAN_POINT ( 'NONE',  ( 10.16000050552179701, -10.16000000000000014, 17.78000050552179445 ) ) ;
#4204=LINE ( 'NONE', #2454, #3159 ) ;
#4207=VECTOR ( 'NONE', #716, 1000.000000000000000 ) ;
#4220=FACE_OUTER_BOUND ( 'NONE', #4641, .T. ) ;
#4222=DIRECTION ( 'NONE',  ( -1.000000000000000000, -0.000000000000000000, -0.000000000000000000 ) ) ;
#4227=DIRECTION ( 'NONE',  ( -1.000000000000000000, -0.000000000000000000, -0.000000000000000000 ) ) ;
#4234=DIRECTION ( 'NONE',  ( -0.000000000000000000, -0.000000000000000000, -1.000000000000000000 ) ) ;
#4239=ORIENTED_EDGE ( 'NONE', *, *, #3402, .T. ) ;
#4252=CARTESIAN_POINT ( 'NONE',  ( 10.16000050552179701, -13.73374999999999879, 10.16000050552179701 ) ) ;
#4255=VERTEX_POINT ( 'NONE', #1256 ) ;
#4259=CARTESIAN_POINT ( 'NONE',  ( 2.540000505521796015, -17.28000000000000114, 17.78000050552179445 ) ) ;
#4265=DIRECTION ( 'NONE',  ( -1.000000000000000000, 0.000000000000000000, 0.000000000000000000 ) ) ;
#4267=DIRECTION ( 'NONE',  ( -1.000000000000000000, 0.000000000000000000, 0.000000000000000000 ) ) ;
#4280=CARTESIAN_POINT ( 'NONE',  ( 17.78000050552179445, -2.539999999999999591, 3.040000505521795571 ) ) ;
#4289=DIRECTION ( 'NONE',  ( 8.673617379884027583E-16, 0.000000000000000000, 1.000000000000000000 ) ) ;
#4299=CARTESIAN_POINT ( 'NONE',  ( 2.540000505521796015, -10.16000000000000014, 10.16000050552179701 ) ) ;
#4300=CARTESIAN_POINT ( 'NONE',  ( 17.78000050552179445, -10.16000000000000014, 10.16000050552179701 ) ) ;
#4302=AXIS2_PLACEMENT_3D ( 'NONE', #3052, #1279, #2700 ) ;
#4318=DIRECTION ( 'NONE',  ( 0.000000000000000000, -0.000000000000000000, -1.000000000000000000 ) ) ;
#4328=PRODUCT_DEFINITION_FORMATION_WITH_SPECIFIED_SOURCE ( 'ANY', '', #3876, .NOT_KNOWN. ) ;
#4334=ORIENTED_EDGE ( 'NONE', *, *, #361, .F. ) ;
#4335=EDGE_CURVE ( 'NONE', #245, #2747, #1637, .T. ) ;
#4336=ORIENTED_EDGE ( 'NONE', *, *, #1303, .T. ) ;
#4344=LINE ( 'NONE', #1880, #4207 ) ;
#4347=CIRCLE ( 'NONE', #2533, 0.5000000000000004441 ) ;
#4348=CYLINDRICAL_SURFACE ( 'NONE', #2155, 0.5000000000000000000 ) ;
#4351=CARTESIAN_POINT ( 'NONE',  ( 3.040000505521796015, -17.28000000000000114, 3.040000505521796015 ) ) ;
#4354=EDGE_CURVE ( 'NONE', #4255, #1351, #229, .T. ) ;
#4355=CARTESIAN_POINT ( 'NONE',  ( 17.28000050552179445, -3.039999999999999591, 3.040000505521796015 ) ) ;
#4356=EDGE_LOOP ( 'NONE', ( #242, #876, #4601, #480 ) ) ;
#4357=AXIS2_PLACEMENT_3D ( 'NONE', #1939, #118, #845 ) ;
#4360=ORIENTED_EDGE ( 'NONE', *, *, #2959, .F. ) ;
#4375=EDGE_CURVE ( 'NONE', #356, #992, #2069, .T. ) ;
#4377=ORIENTED_EDGE ( 'NONE', *, *, #1508, .T. ) ;
#4378=DIRECTION ( 'NONE',  ( -1.000000000000000000, -1.707404996040164265E-16, 0.000000000000000000 ) ) ;
#4397=VERTEX_POINT ( 'NONE', #649 ) ;
#4402=VERTEX_POINT ( 'NONE', #3846 ) ;
#4403=CARTESIAN_POINT ( 'NONE',  ( 13.73375050552179744, -10.16000000000000014, 13.73375050552179744 ) ) ;
#4404=EDGE_CURVE ( 'NONE', #3559, #21, #790, .T. ) ;
#4406=CARTESIAN_POINT ( 'NONE',  ( 17.78000050552179445, -10.16000000000000014, 13.73375050552179744 ) ) ;
#4413=DIRECTION ( 'NONE',  ( 0.000000000000000000, -1.000000000000000000, 0.000000000000000000 ) ) ;
#4415=CYLINDRICAL_SURFACE ( 'NONE', #3825, 3.573749999999999538 ) ;
#4423=ADVANCED_FACE ( 'NONE', ( #2404 ), #253, .F. ) ;
#4426=CARTESIAN_POINT ( 'NONE',  ( 10.16000050552179701, -10.16000000000000014, 17.78000050552179445 ) ) ;
#4435=ADVANCED_FACE ( 'NONE', ( #626 ), #2762, .F. ) ;
#4441=CARTESIAN_POINT ( 'NONE',  ( 3.040000505521796015, -17.28000000000000114, 17.28000050552179445 ) ) ;
#4449=DIRECTION ( 'NONE',  ( -1.000000000000000000, 0.000000000000000000, 0.000000000000000000 ) ) ;
#4450=AXIS2_PLACEMENT_3D ( 'NONE', #1809, #4318, #1852 ) ;
#4451=CYLINDRICAL_SURFACE ( 'NONE', #240, 3.573749999999999538 ) ;
#4452=DIRECTION ( 'NONE',  ( 0.000000000000000000, 1.000000000000000000, 0.000000000000000000 ) ) ;
#4455=ORIENTED_EDGE ( 'NONE', *, *, #3793, .T. ) ;
#4460=ORIENTED_EDGE ( 'NONE', *, *, #2531, .F. ) ;
#4462=DIRECTION ( 'NONE',  ( -1.000000000000000000, 0.000000000000000000, 0.000000000000000000 ) ) ;
#4477=CARTESIAN_POINT ( 'NONE',  ( 6.586250505521797471, -8.066545718530848674, 13.73375050552179566 ) ) ;
#4483=AXIS2_PLACEMENT_3D ( 'NONE', #3752, #129, #3704 ) ;
#4487=CARTESIAN_POINT ( 'NONE',  ( 3.040000505521796015, -2.539999999999999591, 17.78000050552179445 ) ) ;
#4496=ADVANCED_FACE ( 'NONE', ( #3941 ), #762, .T. ) ;
#4508=VECTOR ( 'NONE', #4222, 1000.000000000000000 ) ;
#4523=VECTOR ( 'NONE', #2789, 1000.000000000000000 ) ;
#4525=CARTESIAN_POINT ( 'NONE',  ( 6.586250505521797471, -10.16000000000000014, 2.540000505521796015 ) ) ;
#4528=AXIS2_PLACEMENT_3D ( 'NONE', #941, #2360, #3806 ) ;
#4538=ORIENTED_EDGE ( 'NONE', *, *, #3593, .T. ) ;
#4539=DIRECTION ( 'NONE',  ( -1.000000000000000000, -0.000000000000000000, -0.000000000000000000 ) ) ;
#4557=AXIS2_PLACEMENT_3D ( 'NONE', #1788, #2476, #390 ) ;
#4561=CARTESIAN_POINT ( 'NONE',  ( 10.16000050552179701, -13.73374999999999879, 10.16000050552179701 ) ) ;
#4564=EDGE_LOOP ( 'NONE', ( #2016, #2389, #4336, #3359, #863 ) ) ;
#4568=DIRECTION ( 'NONE',  ( 0.000000000000000000, -1.000000000000000000, 0.000000000000000000 ) ) ;
#4582=EDGE_CURVE ( 'NONE', #2359, #3460, #2222, .T. ) ;
#4586=CARTESIAN_POINT ( 'NONE',  ( 8.066546224052645542, -13.73374999999999524, 12.25345478699094670 ) ) ;
#4597=CARTESIAN_POINT ( 'NONE',  ( 2.540000505521796015, -2.539999999999999591, 3.040000505521795571 ) ) ;
#4601=ORIENTED_EDGE ( 'NONE', *, *, #2409, .F. ) ;
#4603=EDGE_CURVE ( 'NONE', #2813, #1351, #1023, .T. ) ;
#4610=DIRECTION ( 'NONE',  ( -0.000000000000000000, -0.000000000000000000, -1.000000000000000000 ) ) ;
#4611=DIRECTION ( 'NONE',  ( 0.000000000000000000, 0.000000000000000000, 1.000000000000000000 ) ) ;
#4612=LINE ( 'NONE', #3552, #4523 ) ;
#4617=ORIENTED_EDGE ( 'NONE', *, *, #4603, .F. ) ;
#4618=EDGE_LOOP ( 'NONE', ( #875, #2863, #3276, #2537 ) ) ;
#4619=EDGE_CURVE ( 'NONE', #2728, #3496, #1107, .T. ) ;
#4628=DIRECTION ( 'NONE',  ( 0.000000000000000000, 0.000000000000000000, 1.000000000000000000 ) ) ;
#4631=DIRECTION ( 'NONE',  ( 0.000000000000000000, -1.000000000000000000, 0.000000000000000000 ) ) ;
#4641=EDGE_LOOP ( 'NONE', ( #241, #48, #1983 ) ) ;
#4643=ORIENTED_EDGE ( 'NONE', *, *, #177, .T. ) ;
#4644=ADVANCED_FACE ( 'NONE', ( #2945 ), #3679, .T. ) ;
#4645=( NAMED_UNIT ( * ) PLANE_ANGLE_UNIT ( ) SI_UNIT ( $, .RADIAN. ) );
#4648=CARTESIAN_POINT ( 'NONE',  ( 3.040000505521796015, -3.039999999999999591, 17.28000050552179445 ) ) ;
ENDSEC;
END-ISO-10303-21;
